ISO-10303-21;
HEADER;
FILE_DESCRIPTION (('STEP AP214'),
    '1' );
FILE_NAME ('hex flange bolt small_iso_ISO 4162 - M5 x 20 x 20-N.step',
    '2026-10-25T17:17:34',
    ( '' ),
    ( '' ),
    'SwSTEP 2.0',
    'SolidWorks 2026',
    '' );
FILE_SCHEMA (( 'AUTOMOTIVE_DESIGN' ));
ENDSEC;

DATA;
#4=DIRECTION ( 'NONE',  ( -0.000000000000000000, 0.8660254037844382635, 0.5000000000000006661 ) ) ;
#9=CARTESIAN_POINT ( 'NONE',  ( 4.175813232069147674, 2.061359961916367833, 3.570380186727398097 ) ) ;
#25=CARTESIAN_POINT ( 'NONE',  ( 4.055492966679589806, 2.385006769472808319, 3.005124364834396822 ) ) ;
#70=EDGE_CURVE ( 'NONE', #5083, #2374, #8515, .T. ) ;
#82=AXIS2_PLACEMENT_3D ( 'NONE', #16514, #3117, #16700 ) ;
#104=VERTEX_POINT ( 'NONE', #17014 ) ;
#114=AXIS2_PLACEMENT_3D ( 'NONE', #4493, #4109, #5965 ) ;
#129=ORIENTED_EDGE ( 'NONE', *, *, #8766, .F. ) ;
#140=CARTESIAN_POINT ( 'NONE',  ( -5.488773498207864225E-16, -2.859595677584339413, 2.047034997319579386 ) ) ;
#153=CARTESIAN_POINT ( 'NONE',  ( -1.935715396507168721E-15, 2.686816014504566752, 2.346298152288372130 ) ) ;
#168=CARTESIAN_POINT ( 'NONE',  ( 0.000000000000000000, 0.000000000000000000, 0.000000000000000000 ) ) ;
#195=DIRECTION ( 'NONE',  ( 1.000000000000000000, 0.000000000000000000, -0.000000000000000000 ) ) ;
#206=CARTESIAN_POINT ( 'NONE',  ( 4.071447262713887127, 2.020725942163686728, -3.499999999999999556 ) ) ;
#219=CARTESIAN_POINT ( 'NONE',  ( 3.948103430090399879, 3.379418997638482747, 1.146674596026232784 ) ) ;
#234=AXIS2_PLACEMENT_3D ( 'NONE', #19240, #195, #10724 ) ;
#275=CARTESIAN_POINT ( 'NONE',  ( 4.114405500665261783, -2.025575754679711959, -3.508400121684924322 ) ) ;
#287=EDGE_LOOP ( 'NONE', ( #12680, #18333, #2040 ) ) ;
#290=EDGE_CURVE ( 'NONE', #8383, #14066, #13875, .T. ) ;
#305=ORIENTED_EDGE ( 'NONE', *, *, #12340, .T. ) ;
#307=CARTESIAN_POINT ( 'NONE',  ( 3.951447005078452701, -3.704664227300105583, 0.5833333333333329263 ) ) ;
#324=B_SPLINE_CURVE_WITH_KNOTS ( 'NONE', 3,
 ( #1017, #7159, #1300, #2555 ),
 .UNSPECIFIED., .F., .F.,
 ( 4, 4 ),
 ( 0.000000000000000000, 0.002080789711329297104 ),
 .UNSPECIFIED. ) ;
#326=ORIENTED_EDGE ( 'NONE', *, *, #4980, .F. ) ;
#330=ORIENTED_EDGE ( 'NONE', *, *, #12340, .F. ) ;
#332=CARTESIAN_POINT ( 'NONE',  ( 0.000000000000000000, 0.000000000000000000, 2.500000000000000444 ) ) ;
#336=EDGE_LOOP ( 'NONE', ( #9804, #7178, #6008, #18106, #9174, #4508, #17848 ) ) ;
#338=EDGE_CURVE ( 'NONE', #8719, #3780, #14563, .T. ) ;
#349=ADVANCED_FACE ( 'NONE', ( #13762 ), #13787, .T. ) ;
#374=ORIENTED_EDGE ( 'NONE', *, *, #7762, .F. ) ;
#400=DIRECTION ( 'NONE',  ( 0.000000000000000000, 0.000000000000000000, 1.000000000000000000 ) ) ;
#420=CARTESIAN_POINT ( 'NONE',  ( 4.158413352280809328, 4.089743253945649748, -5.087477719935601147E-16 ) ) ;
#434=ADVANCED_FACE ( 'NONE', ( #18369 ), #12304, .F. ) ;
#465=CARTESIAN_POINT ( 'NONE',  ( 4.124214193018025831, -2.028338413290977194, -3.513185186763603696 ) ) ;
#492=CARTESIAN_POINT ( 'NONE',  ( 4.175326769692870421, 2.060699556488908346, -3.569236330973472260 ) ) ;
#519=DIRECTION ( 'NONE',  ( 0.000000000000000000, 0.000000000000000000, 1.000000000000000000 ) ) ;
#523=DIRECTION ( 'NONE',  ( 0.000000000000000000, -1.224646799147353947E-16, 1.000000000000000000 ) ) ;
#559=CARTESIAN_POINT ( 'NONE',  ( 3.880206590543188394, -2.665671387532522196, -2.382921720511056218 ) ) ;
#567=PLANE ( 'NONE',  #8899 ) ;
#581=CARTESIAN_POINT ( 'NONE',  ( 4.114405500665260895, 2.025575754679705298, 3.508400121684924766 ) ) ;
#641=ORIENTED_EDGE ( 'NONE', *, *, #9035, .F. ) ;
#642=CARTESIAN_POINT ( 'NONE',  ( 3.961557105775382670, -1.423285172353652817, 3.500000000000000444 ) ) ;
#701=ORIENTED_EDGE ( 'NONE', *, *, #9112, .F. ) ;
#703=( LENGTH_UNIT ( ) NAMED_UNIT ( * ) SI_UNIT ( .MILLI., .METRE. ) );
#726=AXIS2_PLACEMENT_3D ( 'NONE', #3795, #17290, #18856 ) ;
#802=CARTESIAN_POINT ( 'NONE',  ( 0.1217565302851051218, -2.351289329882176204, -2.927447417349502423 ) ) ;
#856=B_SPLINE_CURVE_WITH_KNOTS ( 'NONE', 3,
 ( #6018, #19210, #16276, #18130, #2978, #19312 ),
 .UNSPECIFIED., .F., .F.,
 ( 4, 2, 4 ),
 ( 0.002044882221487522803, 0.003063384235218489376, 0.004081886248949456383 ),
 .UNSPECIFIED. ) ;
#888=VECTOR ( 'NONE', #17237, 1000.000000000000000 ) ;
#913=EDGE_CURVE ( 'NONE', #11406, #10162, #13170, .T. ) ;
#993=DIRECTION ( 'NONE',  ( 0.000000000000000000, 0.000000000000000000, 1.000000000000000000 ) ) ;
#995=CARTESIAN_POINT ( 'NONE',  ( 4.175813232069151226, -4.122719923832748101, -3.898053888241413974E-16 ) ) ;
#1001=EDGE_CURVE ( 'NONE', #18944, #3020, #12898, .T. ) ;
#1017=CARTESIAN_POINT ( 'NONE',  ( 4.175813232069148562, -2.061359961916374495, -3.570380186727398097 ) ) ;
#1037=CARTESIAN_POINT ( 'NONE',  ( 3.951447005078449148, -1.347150628109125003, 3.500000000000000888 ) ) ;
#1090=DIRECTION ( 'NONE',  ( 0.3420201433256622736, 0.000000000000000000, -0.9396926207859106484 ) ) ;
#1093=CARTESIAN_POINT ( 'NONE',  ( 3.961551342853838698, 2.319461885623308017, 2.982574167880918115 ) ) ;
#1105=ORIENTED_EDGE ( 'NONE', *, *, #2418, .F. ) ;
#1125=MANIFOLD_SOLID_BREP ( 'FlangeHexFillet', #15665 ) ;
#1181=EDGE_LOOP ( 'NONE', ( #9170, #1259, #4978, #13735 ) ) ;
#1182=ORIENTED_EDGE ( 'NONE', *, *, #338, .T. ) ;
#1184=CARTESIAN_POINT ( 'NONE',  ( 4.175075985190098926, -4.120741555260250877, -7.642383270497488377E-15 ) ) ;
#1214=CARTESIAN_POINT ( 'NONE',  ( 5.599999999999998757, 6.472876824008161592E-16, -5.200000000000001066 ) ) ;
#1223=APPLICATION_CONTEXT ( 'automotive_design' ) ;
#1225=CARTESIAN_POINT ( 'NONE',  ( 3.806834918298644066, 8.673617379884035472E-16, 3.500000000000000000 ) ) ;
#1241=CARTESIAN_POINT ( 'NONE',  ( 0.2175679805369682140, -1.691499766289325191, 3.500000000000000000 ) ) ;
#1259=ORIENTED_EDGE ( 'NONE', *, *, #5053, .T. ) ;
#1274=SURFACE_STYLE_USAGE ( .BOTH. , #7318 ) ;
#1279=ORIENTED_EDGE ( 'NONE', *, *, #70, .F. ) ;
#1282=CARTESIAN_POINT ( 'NONE',  ( 3.973514160553462737, 3.435084588004189587, -1.181876024140318115 ) ) ;
#1288=LINE ( 'NONE', #8501, #15479 ) ;
#1300=CARTESIAN_POINT ( 'NONE',  ( 3.973110223768737015, -0.6864646529411585485, -3.565797985667475523 ) ) ;
#1308=CARTESIAN_POINT ( 'NONE',  ( 0.2174200650117542322, -2.185595227304859556, 3.214438021527934897 ) ) ;
#1380=CARTESIAN_POINT ( 'NONE',  ( 4.050823680195224874, 3.779313952391379683, -0.5899027668435159466 ) ) ;
#1388=DIRECTION ( 'NONE',  ( 1.000000000000000000, 0.000000000000000000, -0.000000000000000000 ) ) ;
#1391=VERTEX_POINT ( 'NONE', #8255 ) ;
#1400=CARTESIAN_POINT ( 'NONE',  ( 0.000000000000000000, -3.031088913245531202, 1.750000000000006661 ) ) ;
#1420=EDGE_LOOP ( 'NONE', ( #1182, #9956, #9327, #15515 ) ) ;
#1465=ORIENTED_EDGE ( 'NONE', *, *, #18460, .T. ) ;
#1467=CARTESIAN_POINT ( 'NONE',  ( 4.180345472528542494, 2.086001522971433264, 3.570468649087212398 ) ) ;
#1471=AXIS2_PLACEMENT_3D ( 'NONE', #17709, #7632, #14965 ) ;
#1480=CARTESIAN_POINT ( 'NONE',  ( 4.158806965674306078, 1.986429158307092768, 3.559403772175832259 ) ) ;
#1490=CARTESIAN_POINT ( 'NONE',  ( 3.973110223767137850, 2.263313079739336463E-11, 3.565797985667434222 ) ) ;
#1507=CIRCLE ( 'NONE', #6500, 2.500000000000000444 ) ;
#1517=AXIS2_PLACEMENT_3D ( 'NONE', #3863, #9825, #14312 ) ;
#1543=CARTESIAN_POINT ( 'NONE',  ( 4.175572532730931208, -2.061029303918061828, -3.569807470274388717 ) ) ;
#1546=VERTEX_POINT ( 'NONE', #15734 ) ;
#1573=EDGE_LOOP ( 'NONE', ( #4390, #11414, #129, #16411 ) ) ;
#1579=CARTESIAN_POINT ( 'NONE',  ( 0.000000000000000000, -3.031088913245533867, -1.750000000000002220 ) ) ;
#1594=VERTEX_POINT ( 'NONE', #9 ) ;
#1606=ORIENTED_EDGE ( 'NONE', *, *, #1728, .F. ) ;
#1611=DIRECTION ( 'NONE',  ( 1.000000000000000000, 0.000000000000000000, 0.000000000000000000 ) ) ;
#1635=ORIENTED_EDGE ( 'NONE', *, *, #12151, .F. ) ;
#1637=CARTESIAN_POINT ( 'NONE',  ( 3.948111298835276894, -0.6968132764964359849, -3.500000000000154987 ) ) ;
#1661=CARTESIAN_POINT ( 'NONE',  ( 4.104070371397485317, 2.023683613428365113, -3.505122836902508698 ) ) ;
#1679=CARTESIAN_POINT ( 'NONE',  ( 25.60000000000000142, 2.516649172247811061E-16, -2.055000000000000160 ) ) ;
#1728=EDGE_CURVE ( 'NONE', #18944, #3617, #17178, .T. ) ;
#1750=CARTESIAN_POINT ( 'NONE',  ( 4.093692494532770176, 2.021783646005773427, -3.501831996793853818 ) ) ;
#1753=DIRECTION ( 'NONE',  ( -1.000000000000000000, -0.000000000000000000, -0.000000000000000000 ) ) ;
#1764=CARTESIAN_POINT ( 'NONE',  ( 5.599999999999999645, 0.000000000000000000, 2.500000000000000444 ) ) ;
#1767=ORIENTED_EDGE ( 'NONE', *, *, #12376, .T. ) ;
#1791=AXIS2_PLACEMENT_3D ( 'NONE', #13750, #7986, #6342 ) ;
#1818=CARTESIAN_POINT ( 'NONE',  ( 5.599999999999999645, -2.020725942163688060, 3.500000000000000444 ) ) ;
#1821=ADVANCED_FACE ( 'NONE', ( #14592 ), #17561, .T. ) ;
#1826=CARTESIAN_POINT ( 'NONE',  ( 5.599999999999999645, -4.041451884327388555, 0.000000000000000000 ) ) ;
#1838=ORIENTED_EDGE ( 'NONE', *, *, #290, .F. ) ;
#1850=CARTESIAN_POINT ( 'NONE',  ( 4.071447262713890680, -4.041451884327388555, 0.000000000000000000 ) ) ;
#1860=CARTESIAN_POINT ( 'NONE',  ( 4.086376042167607636, 4.082715877136865679, -0.07147133206918158954 ) ) ;
#1882=DIRECTION ( 'NONE',  ( 0.000000000000000000, 0.000000000000000000, -1.000000000000000000 ) ) ;
#1938=ORIENTED_EDGE ( 'NONE', *, *, #7334, .F. ) ;
#1947=ADVANCED_FACE ( 'NONE', ( #15175 ), #11307, .T. ) ;
#1954=CARTESIAN_POINT ( 'NONE',  ( 4.180345304246198879, 4.135116856707396593, -0.02129519942689974202 ) ) ;
#1956=EDGE_CURVE ( 'NONE', #3617, #7647, #16390, .T. ) ;
#1961=AXIS2_PLACEMENT_3D ( 'NONE', #12311, #3512, #5181 ) ;
#1968=ORIENTED_EDGE ( 'NONE', *, *, #4522, .T. ) ;
#1983=ORIENTED_EDGE ( 'NONE', *, *, #6152, .T. ) ;
#2040=ORIENTED_EDGE ( 'NONE', *, *, #9112, .T. ) ;
#2054=CARTESIAN_POINT ( 'NONE',  ( 4.175813232069148562, 4.122719923832742772, -5.545971589517866732E-16 ) ) ;
#2061=CARTESIAN_POINT ( 'NONE',  ( 25.60000000000000142, 0.000000000000000000, 0.000000000000000000 ) ) ;
#2107=CARTESIAN_POINT ( 'NONE',  ( 4.180345304246200655, -4.135116856707401922, 0.02129519942689706707 ) ) ;
#2190=CARTESIAN_POINT ( 'NONE',  ( 3.878089031707363521, 0.7015470581927524263, 3.500000000000000444 ) ) ;
#2203=CARTESIAN_POINT ( 'NONE',  ( 3.961551342854050528, -2.319461885623371966, -2.982574167880817750 ) ) ;
#2230=EDGE_LOOP ( 'NONE', ( #5939, #17615, #6763 ) ) ;
#2280=CARTESIAN_POINT ( 'NONE',  ( 4.052432342741377980, 1.393590342654233316, 3.567979436357326062 ) ) ;
#2282=CARTESIAN_POINT ( 'NONE',  ( 4.175813232069147674, 2.061359961916367833, 3.570380186727398097 ) ) ;
#2295=ADVANCED_FACE ( 'NONE', ( #6391 ), #2718, .T. ) ;
#2359=CARTESIAN_POINT ( 'NONE',  ( 0.1397371499203162448, 1.362866705341262641, -3.500000000000000444 ) ) ;
#2374=VERTEX_POINT ( 'NONE', #17426 ) ;
#2391=DIRECTION ( 'NONE',  ( 0.000000000000000000, 0.000000000000000000, 1.000000000000000000 ) ) ;
#2400=FACE_BOUND ( 'NONE', #4345, .T. ) ;
#2418=EDGE_CURVE ( 'NONE', #9387, #6061, #324, .T. ) ;
#2450=CARTESIAN_POINT ( 'NONE',  ( 4.071447262713888016, 4.041451884327382338, 0.000000000000000000 ) ) ;
#2457=DIRECTION ( 'NONE',  ( -1.000000000000000000, -0.000000000000000000, -0.000000000000000000 ) ) ;
#2488=ADVANCED_FACE ( 'NONE', ( #18102 ), #13331, .T. ) ;
#2497=CARTESIAN_POINT ( 'NONE',  ( 4.158921614371307918, 1.986121848748763963, -3.559936047944504800 ) ) ;
#2536=CARTESIAN_POINT ( 'NONE',  ( 4.175326769692871309, -2.060699556488903017, 3.569236330973476257 ) ) ;
#2555=CARTESIAN_POINT ( 'NONE',  ( 3.973110223767137850, -2.261515145575163828E-11, -3.565797985667433778 ) ) ;
#2619=CARTESIAN_POINT ( 'NONE',  ( 5.599999999999999645, 2.020725942163686728, -3.499999999999999556 ) ) ;
#2652=DIRECTION ( 'NONE',  ( 1.000000000000000000, 0.000000000000000000, 0.000000000000000000 ) ) ;
#2658=VERTEX_POINT ( 'NONE', #17904 ) ;
#2662=CARTESIAN_POINT ( 'NONE',  ( 0.1217565302851102982, 3.710888496608919507, -0.5725525826504667126 ) ) ;
#2682=ORIENTED_EDGE ( 'NONE', *, *, #4144, .F. ) ;
#2718=TOROIDAL_SURFACE ( 'NONE', #18020, 5.200000000000001066, 0.4999999999999978351 ) ;
#2790=CARTESIAN_POINT ( 'NONE',  ( 4.050480423730738799, 1.376911654797410955, -3.567926555162023394 ) ) ;
#2825=B_SPLINE_CURVE_WITH_KNOTS ( 'NONE', 3,
 ( #8703, #8412, #5597, #17312, #11542, #17694 ),
 .UNSPECIFIED., .F., .F.,
 ( 4, 2, 4 ),
 ( 0.005852013098461907557, 0.006875955139453160392, 0.007899897180444414094 ),
 .UNSPECIFIED. ) ;
#2884=DIRECTION ( 'NONE',  ( 0.000000000000000000, 0.000000000000000000, 1.000000000000000000 ) ) ;
#2895=CIRCLE ( 'NONE', #10702, 2.055000000000000160 ) ;
#2903=ORIENTED_EDGE ( 'NONE', *, *, #12958, .F. ) ;
#2925=ADVANCED_FACE ( 'NONE', ( #7136 ), #5679, .F. ) ;
#2932=ORIENTED_EDGE ( 'NONE', *, *, #3342, .F. ) ;
#2940=CARTESIAN_POINT ( 'NONE',  ( 4.086262629614028086, 1.979770830881088850, 3.570936333571100629 ) ) ;
#2973=ORIENTED_EDGE ( 'NONE', *, *, #16055, .F. ) ;
#2978=CARTESIAN_POINT ( 'NONE',  ( 0.2174200650117588118, -3.876582599186217948, -0.2855619784720692111 ) ) ;
#2997=CARTESIAN_POINT ( 'NONE',  ( 4.180232103119976728, 2.085387772176679366, -3.570466442734698820 ) ) ;
#3012=EDGE_CURVE ( 'NONE', #9387, #104, #4737, .T. ) ;
#3020=VERTEX_POINT ( 'NONE', #3087 ) ;
#3087=CARTESIAN_POINT ( 'NONE',  ( 4.071447262713888016, 4.041451884327382338, 0.000000000000000000 ) ) ;
#3092=CARTESIAN_POINT ( 'NONE',  ( 4.055487192203242941, 1.409979666030558354, -3.568038521265956664 ) ) ;
#3099=EDGE_CURVE ( 'NONE', #1391, #3532, #10613, .T. ) ;
#3117=DIRECTION ( 'NONE',  ( 0.000000000000000000, -0.8660254037844382635, -0.5000000000000008882 ) ) ;
#3140=ORIENTED_EDGE ( 'NONE', *, *, #6608, .T. ) ;
#3177=ORIENTED_EDGE ( 'NONE', *, *, #18192, .T. ) ;
#3188=CARTESIAN_POINT ( 'NONE',  ( 4.050823680195225762, -2.400527758044907589, -2.978030508226147788 ) ) ;
#3210=ORIENTED_EDGE ( 'NONE', *, *, #13066, .T. ) ;
#3230=CARTESIAN_POINT ( 'NONE',  ( 4.132952817037860882, 4.063368025374524350, -1.550749365883601148E-16 ) ) ;
#3257=ORIENTED_EDGE ( 'NONE', *, *, #14718, .F. ) ;
#3284=DIRECTION ( 'NONE',  ( 0.000000000000000000, -1.073081856240829182E-16, -1.000000000000000000 ) ) ;
#3298=FACE_OUTER_BOUND ( 'NONE', #1573, .T. ) ;
#3308=CARTESIAN_POINT ( 'NONE',  ( 4.082498951862918446, 2.020725942163685840, -3.500000000000001332 ) ) ;
#3319=CARTESIAN_POINT ( 'NONE',  ( 4.030867648404801606, 3.732851566702016122, 0.5345114293586211707 ) ) ;
#3333=ORIENTED_EDGE ( 'NONE', *, *, #5566, .T. ) ;
#3342=EDGE_CURVE ( 'NONE', #12012, #4621, #15855, .T. ) ;
#3351=( BOUNDED_SURFACE ( )  B_SPLINE_SURFACE ( 3, 2, ( 
 ( #13920, #6412, #5047 ),
 ( #2203, #16670, #4854 ),
 ( #559, #3378, #9528 ),
 ( #10989, #5141, #10799 ),
 ( #8067, #18427, #15494 ),
 ( #15595, #18623, #2107 ) ),
 .UNSPECIFIED., .F., .F., .F. ) 
 B_SPLINE_SURFACE_WITH_KNOTS ( ( 4, 2, 4 ),
 ( 3, 3 ),
 ( 0.01651999345535507327, 0.01858032176739836741, 0.02064065007944166155 ),
 ( 0.000000000000000000, 1.000000000000000000 ),
 .UNSPECIFIED. ) 
 GEOMETRIC_REPRESENTATION_ITEM ( )  RATIONAL_B_SPLINE_SURFACE ( (
 ( 1.000000000000000000, 0.8047781103519393575, 1.000000000000000000),
 ( 1.000000000000000000, 0.8123785825613525358, 1.000000000000000000),
 ( 1.000000000000000000, 0.8190671539776085419, 1.000000000000000000),
 ( 1.000000000000000000, 0.8192352254847058424, 1.000000000000000000),
 ( 1.000000000000000000, 0.8126129677202444945, 1.000000000000000000),
 ( 1.000000000000000000, 0.8047712537969730073, 1.000000000000000000) ) ) 
 REPRESENTATION_ITEM ( '' )  SURFACE ( )  );
#3369=CARTESIAN_POINT ( 'NONE',  ( 4.630153689607048761, 6.577590292450083844E-16, 5.371010071662833063 ) ) ;
#3375=PRODUCT_DEFINITION_CONTEXT ( 'detailed design', #1223, 'design' ) ;
#3378=CARTESIAN_POINT ( 'NONE',  ( 3.950241966888159428, -2.668221755852938415, -2.378504353001738902 ) ) ;
#3380=CARTESIAN_POINT ( 'NONE',  ( 4.158413352280809328, -2.044871626972829759, -3.541821552872960854 ) ) ;
#3381=EDGE_CURVE ( 'NONE', #15492, #13429, #10568, .T. ) ;
#3387=CARTESIAN_POINT ( 'NONE',  ( 5.599999999999998757, 0.000000000000000000, 5.200000000000001066 ) ) ;
#3400=PLANE ( 'NONE',  #15847 ) ;
#3428=CARTESIAN_POINT ( 'NONE',  ( 4.093692494532767512, 4.043567292011554848, -1.127116027090594736E-16 ) ) ;
#3488=CARTESIAN_POINT ( 'NONE',  ( 4.071447262713887127, 2.020725942163688504, 3.500000000000000000 ) ) ;
#3496=EDGE_CURVE ( 'NONE', #3020, #14066, #11714, .T. ) ;
#3498=CARTESIAN_POINT ( 'NONE',  ( 3.951447005078452701, 3.704664227300100698, -0.5833333333333330373 ) ) ;
#3500=ORIENTED_EDGE ( 'NONE', *, *, #19165, .F. ) ;
#3512=DIRECTION ( 'NONE',  ( 1.000000000000000000, 0.000000000000000000, -0.000000000000000000 ) ) ;
#3532=VERTEX_POINT ( 'NONE', #15253 ) ;
#3533=ORIENTED_EDGE ( 'NONE', *, *, #16809, .F. ) ;
#3537=CARTESIAN_POINT ( 'NONE',  ( 4.175813232069151226, -4.122719923832748101, -3.898053888241413974E-16 ) ) ;
#3575=PRODUCT_DEFINITION_SHAPE ( 'NONE', 'NONE',  #4398 ) ;
#3581=EDGE_LOOP ( 'NONE', ( #8099, #9700, #15443, #10797 ) ) ;
#3617=VERTEX_POINT ( 'NONE', #7825 ) ;
#3629=CARTESIAN_POINT ( 'NONE',  ( 3.972709601346593011, -2.746729940827192795, 2.374099244652734697 ) ) ;
#3630=COLOUR_RGB ( '',1.000000000000000000, 0.9490196078431372140, 0.9098039215686274384 ) ;
#3644=CARTESIAN_POINT ( 'NONE',  ( 4.086262841041386373, 2.102637316508698451, -3.499999999999999556 ) ) ;
#3655=VECTOR ( 'NONE', #13536, 1000.000000000000000 ) ;
#3722=CARTESIAN_POINT ( 'NONE',  ( 4.124214193018032049, -2.028338413290972753, 3.513185186763607248 ) ) ;
#3744=CARTESIAN_POINT ( 'NONE',  ( 4.030875481281934292, 1.403567514398448068, 3.500000000000000000 ) ) ;
#3751=CARTESIAN_POINT ( 'NONE',  ( 4.175813232069147674, 2.061359961916367833, 3.570380186727398097 ) ) ;
#3779=CARTESIAN_POINT ( 'NONE',  ( 4.175075985190095373, 2.060370777630105898, 3.568666869285574972 ) ) ;
#3780=VERTEX_POINT ( 'NONE', #16199 ) ;
#3795=CARTESIAN_POINT ( 'NONE',  ( 25.60000000000000142, 0.000000000000000000, 0.000000000000000000 ) ) ;
#3803=ORIENTED_EDGE ( 'NONE', *, *, #3099, .T. ) ;
#3812=CARTESIAN_POINT ( 'NONE',  ( 3.974175853610053100, -3.450041667725632699, 1.156004144284124457 ) ) ;
#3826=CIRCLE ( 'NONE', #1961, 3.500000000000000000 ) ;
#3850=B_SPLINE_CURVE_WITH_KNOTS ( 'NONE', 3,
 ( #13565, #15425, #492, #9171, #16606, #18367, #18081, #9460, #9074, #7517, #4592, #10550, #1661, #1750, #3308, #206 ),
 .UNSPECIFIED., .F., .F.,
 ( 4, 3, 3, 3, 3, 4 ),
 ( -2.111273352580990396E-06, 0.000000000000000000, 3.519286887793134604E-05, 7.191842652045515611E-05, 0.0001049868727088832553, 0.0001382836236814611892 ),
 .UNSPECIFIED. ) ;
#3863=CARTESIAN_POINT ( 'NONE',  ( 4.630153689607048761, 0.000000000000000000, 0.000000000000000000 ) ) ;
#3875=CARTESIAN_POINT ( 'NONE',  ( 4.630153689607048761, 0.000000000000000000, 0.000000000000000000 ) ) ;
#3927=DIRECTION ( 'NONE',  ( 0.000000000000000000, 0.000000000000000000, -1.000000000000000000 ) ) ;
#3937=ORIENTED_EDGE ( 'NONE', *, *, #18192, .F. ) ;
#3962=ADVANCED_FACE ( 'NONE', ( #18893 ), #12402, .T. ) ;
#3967=CARTESIAN_POINT ( 'NONE',  ( 3.878096787214571073, 2.680238624820943549, -2.357690525401585191 ) ) ;
#3968=CARTESIAN_POINT ( 'NONE',  ( 4.175813232069148562, 4.122719923832742772, -5.545971589517866732E-16 ) ) ;
#3976=CARTESIAN_POINT ( 'NONE',  ( 4.175813232069147674, 2.061359961916367833, 3.570380186727398097 ) ) ;
#3990=EDGE_CURVE ( 'NONE', #3532, #18754, #8811, .T. ) ;
#4008=CONICAL_SURFACE ( 'NONE', #1517, 5.371010071662833063, 1.221730476396037490 ) ;
#4009=PRESENTATION_STYLE_ASSIGNMENT (( #1274 ) ) ;
#4046=CARTESIAN_POINT ( 'NONE',  ( -2.245091464683528031E-15, 3.375361811986501870, -1.153701847711632089 ) ) ;
#4058=CARTESIAN_POINT ( 'NONE',  ( 4.071447262713887127, 2.020725942163688504, 3.500000000000000000 ) ) ;
#4082=CARTESIAN_POINT ( 'NONE',  ( 3.806834918298647619, -3.031088913245542749, -1.750000000000000222 ) ) ;
#4102=FILL_AREA_STYLE_COLOUR ( '', #3630 ) ;
#4109=DIRECTION ( 'NONE',  ( -1.000000000000000000, -0.000000000000000000, -0.000000000000000000 ) ) ;
#4144=EDGE_CURVE ( 'NONE', #7899, #2374, #9811, .T. ) ;
#4145=PLANE ( 'NONE',  #12067 ) ;
#4147=DIRECTION ( 'NONE',  ( 0.000000000000000000, 0.000000000000000000, 1.000000000000000000 ) ) ;
#4259=FACE_OUTER_BOUND ( 'NONE', #17687, .T. ) ;
#4278=CARTESIAN_POINT ( 'NONE',  ( 0.000000000000000000, 3.755786496842896592E-16, -3.499999999999999556 ) ) ;
#4294=CONICAL_SURFACE ( 'NONE', #18974, 3.500000000000000000, 1.047197551196600296 ) ;
#4303=FACE_OUTER_BOUND ( 'NONE', #11025, .T. ) ;
#4315=AXIS2_PLACEMENT_3D ( 'NONE', #15548, #11138, #9381 ) ;
#4344=ADVANCED_FACE ( 'NONE', ( #16825 ), #17416, .T. ) ;
#4345=EDGE_LOOP ( 'NONE', ( #9685, #10871 ) ) ;
#4373=EDGE_CURVE ( 'NONE', #10751, #7830, #13299, .T. ) ;
#4386=FACE_OUTER_BOUND ( 'NONE', #15695, .T. ) ;
#4390=ORIENTED_EDGE ( 'NONE', *, *, #8503, .T. ) ;
#4398=PRODUCT_DEFINITION ( 'UNKNOWN', '', #19243, #3375 ) ;
#4401=CARTESIAN_POINT ( 'NONE',  ( 4.175813232069148562, 4.122719923832742772, -5.545971589517866732E-16 ) ) ;
#4408=CARTESIAN_POINT ( 'NONE',  ( 0.000000000000000000, 3.031088913245533867, 1.750000000000002887 ) ) ;
#4444=DIRECTION ( 'NONE',  ( 0.000000000000000000, 0.000000000000000000, -1.000000000000000000 ) ) ;
#4448=CARTESIAN_POINT ( 'NONE',  ( 0.000000000000000000, 0.000000000000000000, 0.000000000000000000 ) ) ;
#4471=CARTESIAN_POINT ( 'NONE',  ( 3.961545574370306966, 1.423222908132971476, -3.499999999999999556 ) ) ;
#4482=DIRECTION ( 'NONE',  ( 0.000000000000000000, -0.5000000000000006661, 0.8660254037844382635 ) ) ;
#4493=CARTESIAN_POINT ( 'NONE',  ( 25.15499999999999758, 0.000000000000000000, 0.000000000000000000 ) ) ;
#4495=CARTESIAN_POINT ( 'NONE',  ( 4.175813232069151226, -4.122719923832748101, -3.898053888241413974E-16 ) ) ;
#4508=ORIENTED_EDGE ( 'NONE', *, *, #13701, .T. ) ;
#4517=ORIENTED_EDGE ( 'NONE', *, *, #4373, .T. ) ;
#4522=EDGE_CURVE ( 'NONE', #3020, #5869, #5402, .T. ) ;
#4577=EDGE_CURVE ( 'NONE', #104, #3780, #18687, .T. ) ;
#4592=CARTESIAN_POINT ( 'NONE',  ( 4.124214193018032049, 2.028338413290970976, -3.513185186763606804 ) ) ;
#4606=CARTESIAN_POINT ( 'NONE',  ( 4.033901012036126943, 2.321269032827665058, 2.979444097106977107 ) ) ;
#4611=AXIS2_PLACEMENT_3D ( 'NONE', #16049, #2652, #9900 ) ;
#4615=CARTESIAN_POINT ( 'NONE',  ( 3.973110223765528026, -0.6902454861566470479, 3.565797985667392034 ) ) ;
#4621=VERTEX_POINT ( 'NONE', #6837 ) ;
#4646=ORIENTED_EDGE ( 'NONE', *, *, #13701, .F. ) ;
#4737=B_SPLINE_CURVE_WITH_KNOTS ( 'NONE', 3,
 ( #10419, #1543, #13823, #7491, #18143, #6033, #3380, #13446, #16383, #12275, #465, #275, #7586, #15197, #4856, #13732 ),
 .UNSPECIFIED., .F., .F.,
 ( 4, 3, 3, 3, 3, 4 ),
 ( -2.111273352581839123E-06, 0.000000000000000000, 3.519286887794243878E-05, 7.191842652046502235E-05, 0.0001049868727088876057, 0.0001382836236814605387 ),
 .UNSPECIFIED. ) ;
#4776=EDGE_LOOP ( 'NONE', ( #11438, #13396 ) ) ;
#4782=PLANE ( 'NONE',  #234 ) ;
#4797=CARTESIAN_POINT ( 'NONE',  ( 4.104070371397484429, -4.047367226856742661, 2.300149018892232304E-16 ) ) ;
#4806=CARTESIAN_POINT ( 'NONE',  ( 5.599999999999999645, 3.061616997868383634E-16, -2.500000000000000444 ) ) ;
#4854=CARTESIAN_POINT ( 'NONE',  ( 4.055492966679554279, -2.385006769472701738, -3.005124364834346196 ) ) ;
#4856=CARTESIAN_POINT ( 'NONE',  ( 4.082498951862917558, -2.020725942163695166, -3.500000000000000000 ) ) ;
#4888=CARTESIAN_POINT ( 'NONE',  ( 4.093692494532770176, -4.043567292011561065, 2.300149018892232304E-16 ) ) ;
#4911=B_SPLINE_CURVE_WITH_KNOTS ( 'NONE', 3,
 ( #10005, #2662, #4046, #17725 ),
 .UNSPECIFIED., .F., .F.,
 ( 4, 4 ),
 ( 2.380739282179989060E-07, 0.002044882221487534513 ),
 .UNSPECIFIED. ) ;
#4912=ORIENTED_EDGE ( 'NONE', *, *, #7854, .F. ) ;
#4977=DIRECTION ( 'NONE',  ( -1.000000000000000000, 0.000000000000000000, -0.000000000000000000 ) ) ;
#4978=ORIENTED_EDGE ( 'NONE', *, *, #3990, .T. ) ;
#4980=EDGE_CURVE ( 'NONE', #5083, #11132, #12177, .T. ) ;
#4987=CARTESIAN_POINT ( 'NONE',  ( 4.071447262713887127, -2.020725942163688060, 3.500000000000000444 ) ) ;
#5032=ORIENTED_EDGE ( 'NONE', *, *, #6388, .T. ) ;
#5047=CARTESIAN_POINT ( 'NONE',  ( 4.180231891692620216, -2.049421325483212097, -3.591231015387277292 ) ) ;
#5053=EDGE_CURVE ( 'NONE', #13429, #3532, #11173, .T. ) ;
#5083=VERTEX_POINT ( 'NONE', #9927 ) ;
#5097=CARTESIAN_POINT ( 'NONE',  ( 4.104070371397481765, 4.047367226856737332, -1.119160662980175398E-16 ) ) ;
#5106=CARTESIAN_POINT ( 'NONE',  ( 4.165266963751927065, -2.049631966911921843, 3.550066703508780286 ) ) ;
#5128=CARTESIAN_POINT ( 'NONE',  ( 3.950250160040163383, -0.7258013381034684741, 3.499999999999845013 ) ) ;
#5141=CARTESIAN_POINT ( 'NONE',  ( 3.948103430090712962, -3.379418997638331312, -1.146674596027277060 ) ) ;
#5181=DIRECTION ( 'NONE',  ( 0.000000000000000000, 0.000000000000000000, -1.000000000000000000 ) ) ;
#5190=ORIENTED_EDGE ( 'NONE', *, *, #12122, .F. ) ;
#5225=CARTESIAN_POINT ( 'NONE',  ( 0.1388410611046075049, 2.351840044243034722, -2.926493552096022466 ) ) ;
#5230=ADVANCED_FACE ( 'NONE', ( #11288 ), #4008, .T. ) ;
#5297=ORIENTED_EDGE ( 'NONE', *, *, #16809, .T. ) ;
#5328=CARTESIAN_POINT ( 'NONE',  ( -2.378468515890074563E-15, 2.859595677584338080, -2.047034997319574945 ) ) ;
#5392=ADVANCED_FACE ( 'NONE', ( #16075 ), #8994, .T. ) ;
#5402=B_SPLINE_CURVE_WITH_KNOTS ( 'NONE', 3,
 ( #15422, #3498, #6347, #16796, #13664 ),
 .UNSPECIFIED., .F., .F.,
 ( 4, 1, 4 ),
 ( 3.224213076541126624E-34, 0.002020725942163690940, 0.004041451884327381880 ),
 .UNSPECIFIED. ) ;
#5449=( BOUNDED_SURFACE ( )  B_SPLINE_SURFACE ( 3, 2, ( 
 ( #10219, #14318, #11297 ),
 ( #5546, #11395, #17358 ),
 ( #9833, #14605, #8551 ),
 ( #3967, #9933, #7095 ),
 ( #17264, #16185, #17550 ),
 ( #15891, #2497, #7188 ) ),
 .UNSPECIFIED., .F., .F., .F. ) 
 B_SPLINE_SURFACE_WITH_KNOTS ( ( 4, 2, 4 ),
 ( 3, 3 ),
 ( 0.01651999345535504551, 0.01858032176739834312, 0.02064065007944163727 ),
 ( 0.000000000000000000, 1.000000000000000000 ),
 .UNSPECIFIED. ) 
 GEOMETRIC_REPRESENTATION_ITEM ( )  RATIONAL_B_SPLINE_SURFACE ( (
 ( 1.000000000000000000, 0.8047781103519391355, 1.000000000000000000),
 ( 1.000000000000000000, 0.8123785825602164445, 1.000000000000000000),
 ( 1.000000000000000000, 0.8190671539791195555, 1.000000000000000000),
 ( 1.000000000000000000, 0.8192352254831950509, 1.000000000000000000),
 ( 1.000000000000000000, 0.8126129677213795865, 1.000000000000000000),
 ( 1.000000000000000000, 0.8047712537969733404, 1.000000000000000000) ) ) 
 REPRESENTATION_ITEM ( '' )  SURFACE ( )  );
#5459=CARTESIAN_POINT ( 'NONE',  ( 0.1217565302851127407, -3.710888496608923948, 0.5725525826504677118 ) ) ;
#5467=CARTESIAN_POINT ( 'NONE',  ( 4.071447262713890680, -4.041451884327388555, 0.000000000000000000 ) ) ;
#5489=DIRECTION ( 'NONE',  ( 0.000000000000000000, -0.5000000000000012212, -0.8660254037844380415 ) ) ;
#5493=CARTESIAN_POINT ( 'NONE',  ( 3.972066048304732533, -2.740530939476237826, 2.384802634787742903 ) ) ;
#5494=AXIS2_PLACEMENT_3D ( 'NONE', #4448, #17749, #2884 ) ;
#5497=CARTESIAN_POINT ( 'NONE',  ( 4.175813232069148562, -2.061359961916374495, -3.570380186727398097 ) ) ;
#5546=CARTESIAN_POINT ( 'NONE',  ( 3.961551342853556257, 3.742715940867794355, -0.5174258321190280396 ) ) ;
#5555=EDGE_LOOP ( 'NONE', ( #2903, #16505, #8121, #701, #10451 ) ) ;
#5562=CARTESIAN_POINT ( 'NONE',  ( 0.000000000000000000, 3.061616997868383634E-16, -2.500000000000000444 ) ) ;
#5566=EDGE_CURVE ( 'NONE', #1546, #13533, #6780, .T. ) ;
#5597=CARTESIAN_POINT ( 'NONE',  ( 0.03027795055833725976, 0.6888063905328605241, 3.500000000000000444 ) ) ;
#5630=CARTESIAN_POINT ( 'NONE',  ( 4.071447262713887127, -2.020725942163688060, 3.500000000000000444 ) ) ;
#5635=DIRECTION ( 'NONE',  ( 1.000000000000000000, 0.000000000000000000, 0.000000000000000000 ) ) ;
#5653=ADVANCED_FACE ( 'NONE', ( #4303 ), #18139, .F. ) ;
#5675=( NAMED_UNIT ( * ) SI_UNIT ( $, .STERADIAN. ) SOLID_ANGLE_UNIT ( ) );
#5679=PLANE ( 'NONE',  #11770 ) ;
#5682=EDGE_LOOP ( 'NONE', ( #18585, #1968, #18788, #8286, #10927 ) ) ;
#5696=AXIS2_PLACEMENT_3D ( 'NONE', #18059, #9146, #15110 ) ;
#5713=FACE_OUTER_BOUND ( 'NONE', #17639, .T. ) ;
#5747=CARTESIAN_POINT ( 'NONE',  ( 0.1381419387119273146, -1.355287006778810310, -3.499999999999999556 ) ) ;
#5814=ORIENTED_EDGE ( 'NONE', *, *, #8205, .T. ) ;
#5835=ORIENTED_EDGE ( 'NONE', *, *, #12376, .F. ) ;
#5869=VERTEX_POINT ( 'NONE', #16699 ) ;
#5882=AXIS2_PLACEMENT_3D ( 'NONE', #17351, #18528, #8547 ) ;
#5939=ORIENTED_EDGE ( 'NONE', *, *, #15263, .T. ) ;
#5965=DIRECTION ( 'NONE',  ( 0.000000000000000000, 0.000000000000000000, 1.000000000000000000 ) ) ;
#6008=ORIENTED_EDGE ( 'NONE', *, *, #12151, .T. ) ;
#6011=STYLED_ITEM('',(#19371),#1125);
#6018=CARTESIAN_POINT ( 'NONE',  ( 0.000000000000000000, -3.031088913245533867, -1.750000000000002220 ) ) ;
#6033=CARTESIAN_POINT ( 'NONE',  ( 4.165266963751924401, -2.049631966911926284, -3.550066703508774069 ) ) ;
#6061=VERTEX_POINT ( 'NONE', #8288 ) ;
#6080=APPLICATION_CONTEXT ( 'automotive_design' ) ;
#6090=CARTESIAN_POINT ( 'NONE',  ( 0.3126073911696412022, -2.020725942163688504, 3.500000000000000444 ) ) ;
#6094=CARTESIAN_POINT ( 'NONE',  ( 0.000000000000000000, 3.755786496842896592E-16, -3.499999999999999556 ) ) ;
#6144=PLANE ( 'NONE',  #7705 ) ;
#6152=EDGE_CURVE ( 'NONE', #13276, #10751, #6468, .T. ) ;
#6159=CARTESIAN_POINT ( 'NONE',  ( 3.806834918298644954, -3.031088913245539640, 1.750000000000000666 ) ) ;
#6193=VECTOR ( 'NONE', #13734, 1000.000000000000000 ) ;
#6218=DIRECTION ( 'NONE',  ( 0.000000000000000000, 0.000000000000000000, -1.000000000000000000 ) ) ;
#6246=ADVANCED_FACE ( 'NONE', ( #17955 ), #13394, .F. ) ;
#6254=ORIENTED_EDGE ( 'NONE', *, *, #17204, .F. ) ;
#6312=EDGE_CURVE ( 'NONE', #8719, #9387, #12760, .T. ) ;
#6328=CARTESIAN_POINT ( 'NONE',  ( 4.050536630291691864, -3.778525289263166442, -0.5912575323401421112 ) ) ;
#6331=LINE ( 'NONE', #1826, #888 ) ;
#6342=DIRECTION ( 'NONE',  ( 0.000000000000000000, 0.000000000000000000, 1.000000000000000000 ) ) ;
#6347=CARTESIAN_POINT ( 'NONE',  ( 3.806834918298644066, 3.031088913245536531, -1.749999999999997558 ) ) ;
#6349=ORIENTED_EDGE ( 'NONE', *, *, #5053, .F. ) ;
#6388=EDGE_CURVE ( 'NONE', #17929, #7647, #8481, .T. ) ;
#6391=FACE_OUTER_BOUND ( 'NONE', #8561, .T. ) ;
#6412=CARTESIAN_POINT ( 'NONE',  ( 4.158806965674307854, -1.986429158307096543, -3.559403772175836256 ) ) ;
#6445=CARTESIAN_POINT ( 'NONE',  ( 3.951447005078450037, -2.357513599190973252, 2.916666666666666963 ) ) ;
#6461=CARTESIAN_POINT ( 'NONE',  ( 4.175075985190097150, 4.120741555260244660, 1.921191574886163109E-14 ) ) ;
#6468=B_SPLINE_CURVE_WITH_KNOTS ( 'NONE', 3,
 ( #4278, #7497, #8767, #5747, #19129, #14717 ),
 .UNSPECIFIED., .F., .F.,
 ( 4, 2, 4 ),
 ( 0.01308430721348208606, 0.01410661710602281044, 0.01512892699856353655 ),
 .UNSPECIFIED. ) ;
#6500=AXIS2_PLACEMENT_3D ( 'NONE', #11549, #19073, #3927 ) ;
#6529=DIRECTION ( 'NONE',  ( -1.000000000000000000, -0.000000000000000000, -0.000000000000000000 ) ) ;
#6554=CARTESIAN_POINT ( 'NONE',  ( 3.973110223767137850, 2.263313079739336463E-11, 3.565797985667434222 ) ) ;
#6592=CARTESIAN_POINT ( 'NONE',  ( 4.033906725094790424, -1.419670120618843789, 3.500000000000000888 ) ) ;
#6605=FACE_OUTER_BOUND ( 'NONE', #1420, .T. ) ;
#6608=EDGE_CURVE ( 'NONE', #6061, #8383, #8087, .T. ) ;
#6691=CARTESIAN_POINT ( 'NONE',  ( 0.3126073911696399255, 2.020725942163686728, -3.499999999999999556 ) ) ;
#6712=CARTESIAN_POINT ( 'NONE',  ( 5.599999999999999645, 4.041451884327382338, 2.749426538070117193E-16 ) ) ;
#6759=CIRCLE ( 'NONE', #17982, 2.500000000000000444 ) ;
#6763=ORIENTED_EDGE ( 'NONE', *, *, #11143, .T. ) ;
#6764=CARTESIAN_POINT ( 'NONE',  ( 4.033901012036456457, -3.740908793663545673, 0.5205559028932933430 ) ) ;
#6780=B_SPLINE_CURVE_WITH_KNOTS ( 'NONE', 3,
 ( #12634, #5328, #12538, #5225, #12834, #6691 ),
 .UNSPECIFIED., .F., .F.,
 ( 4, 2, 4 ),
 ( 0.002044882221487534513, 0.003063384235218497183, 0.004081886248949459853 ),
 .UNSPECIFIED. ) ;
#6789=CIRCLE ( 'NONE', #13675, 5.371010071662833063 ) ;
#6792=EDGE_CURVE ( 'NONE', #14066, #1594, #11827, .T. ) ;
#6813=EDGE_LOOP ( 'NONE', ( #3333, #19226, #3177 ) ) ;
#6829=AXIS2_PLACEMENT_3D ( 'NONE', #3875, #11399, #14507 ) ;
#6830=CARTESIAN_POINT ( 'NONE',  ( 4.165266963751923512, 2.049631966911918735, 3.550066703508774957 ) ) ;
#6837=CARTESIAN_POINT ( 'NONE',  ( 4.630153689607048761, 0.000000000000000000, -5.371010071662833063 ) ) ;
#6862=CARTESIAN_POINT ( 'NONE',  ( 3.878096787214261987, -2.680238624821020377, 2.357690525401458181 ) ) ;
#6863=CARTESIAN_POINT ( 'NONE',  ( 4.170895651974601215, -2.054890354522714180, 3.559174498016426824 ) ) ;
#6897=CARTESIAN_POINT ( 'NONE',  ( 4.030859730898683324, -1.403482646610935358, -3.500000000000000000 ) ) ;
#6951=CARTESIAN_POINT ( 'NONE',  ( 4.086376042167606748, -1.979461949354205164, 3.571471332069182658 ) ) ;
#6952=CIRCLE ( 'NONE', #9429, 3.500000000000000000 ) ;
#6964=CARTESIAN_POINT ( 'NONE',  ( 0.02993401039713615083, 3.373851915354614928, 1.156317065392238774 ) ) ;
#6997=DIRECTION ( 'NONE',  ( 0.000000000000000000, 0.000000000000000000, -1.000000000000000000 ) ) ;
#7073=CARTESIAN_POINT ( 'NONE',  ( 5.599999999999998757, 0.000000000000000000, 0.000000000000000000 ) ) ;
#7082=CARTESIAN_POINT ( 'NONE',  ( 25.60000000000000142, 0.000000000000000000, 0.000000000000000000 ) ) ;
#7095=CARTESIAN_POINT ( 'NONE',  ( 3.972066048304737418, 2.740530939476172989, -2.384802634787877018 ) ) ;
#7097=CARTESIAN_POINT ( 'NONE',  ( 4.175813232069146785, 2.061359961916366057, -3.570380186727397653 ) ) ;
#7132=( LENGTH_UNIT ( ) NAMED_UNIT ( * ) SI_UNIT ( .MILLI., .METRE. ) );
#7136=FACE_OUTER_BOUND ( 'NONE', #5682, .T. ) ;
#7139=EDGE_LOOP ( 'NONE', ( #18390, #8923, #18174, #9009 ) ) ;
#7142=CARTESIAN_POINT ( 'NONE',  ( 3.972709601346591235, 2.746729940827189242, -2.374099244652734697 ) ) ;
#7159=CARTESIAN_POINT ( 'NONE',  ( 4.050880675075948290, -1.379097446046192887, -3.567934390854430760 ) ) ;
#7177=CARTESIAN_POINT ( 'NONE',  ( 4.086375874528100027, -2.103253014742892280, -3.500000000000000000 ) ) ;
#7178=ORIENTED_EDGE ( 'NONE', *, *, #4144, .T. ) ;
#7188=CARTESIAN_POINT ( 'NONE',  ( 4.180345304246197102, 2.049116244671343345, -3.591763845239307251 ) ) ;
#7193=CARTESIAN_POINT ( 'NONE',  ( 0.000000000000000000, 3.755786496842902015E-16, 3.500000000000000000 ) ) ;
#7269=CARTESIAN_POINT ( 'NONE',  ( 4.180345136606690382, -2.085999704580137060, -3.570468642550115757 ) ) ;
#7274=VECTOR ( 'NONE', #6529, 1000.000000000000000 ) ;
#7308=EDGE_CURVE ( 'NONE', #15492, #1391, #13492, .T. ) ;
#7318=SURFACE_SIDE_STYLE ('',( #19246 ) ) ;
#7334=EDGE_CURVE ( 'NONE', #13533, #13276, #14823, .T. ) ;
#7341=CARTESIAN_POINT ( 'NONE',  ( 0.000000000000000000, 0.000000000000000000, 0.000000000000000000 ) ) ;
#7353=CARTESIAN_POINT ( 'NONE',  ( 0.02993401039713761494, -2.688325911136454138, 2.343682934607770108 ) ) ;
#7412=ORIENTED_EDGE ( 'NONE', *, *, #6152, .F. ) ;
#7444=CARTESIAN_POINT ( 'NONE',  ( 4.175813232069147674, -2.061359961916367833, 3.570380186727398542 ) ) ;
#7455=DIRECTION ( 'NONE',  ( -0.000000000000000000, 1.000000000000000000, 1.224646799147353207E-16 ) ) ;
#7491=CARTESIAN_POINT ( 'NONE',  ( 4.175075985190096262, -2.060370777630129435, -3.568666869285562981 ) ) ;
#7497=CARTESIAN_POINT ( 'NONE',  ( -1.639008752937070663E-16, -0.3420925509381497198, -3.499999999999999112 ) ) ;
#7517=CARTESIAN_POINT ( 'NONE',  ( 4.132952817037867987, 2.031684012687260399, -3.518979934899751694 ) ) ;
#7520=CARTESIAN_POINT ( 'NONE',  ( 4.170895651974602991, -4.109780709045316449, 3.824548179337212366E-14 ) ) ;
#7586=CARTESIAN_POINT ( 'NONE',  ( 4.104070371397481765, -2.023683613428372219, -3.505122836902507366 ) ) ;
#7632=DIRECTION ( 'NONE',  ( 1.000000000000000000, 0.000000000000000000, 0.000000000000000000 ) ) ;
#7647=VERTEX_POINT ( 'NONE', #4408 ) ;
#7699=B_SPLINE_CURVE_WITH_KNOTS ( 'NONE', 3,
 ( #3751, #12264, #11078, #8251 ),
 .UNSPECIFIED., .F., .F.,
 ( 4, 4 ),
 ( 0.000000000000000000, 0.002080789711329271950 ),
 .UNSPECIFIED. ) ;
#7705=AXIS2_PLACEMENT_3D ( 'NONE', #15122, #4, #4482 ) ;
#7729=CARTESIAN_POINT ( 'NONE',  ( 4.071447262713888016, 4.041451884327382338, 0.000000000000000000 ) ) ;
#7731=CARTESIAN_POINT ( 'NONE',  ( 4.050480423730737911, -1.376911654797406959, 3.567926555162024282 ) ) ;
#7762=EDGE_CURVE ( 'NONE', #17929, #10812, #6952, .T. ) ;
#7778=CARTESIAN_POINT ( 'NONE',  ( 25.60000000000000142, 0.000000000000000000, 2.055000000000000160 ) ) ;
#7808=CARTESIAN_POINT ( 'NONE',  ( 4.082498951862920222, -4.041451884327388555, -2.280731272670711599E-17 ) ) ;
#7825=CARTESIAN_POINT ( 'NONE',  ( 0.3126073911696408136, 2.020725942163688060, 3.500000000000000000 ) ) ;
#7830=VERTEX_POINT ( 'NONE', #1579 ) ;
#7834=DIRECTION ( 'NONE',  ( -1.000000000000000000, -0.000000000000000000, -0.000000000000000000 ) ) ;
#7854=EDGE_CURVE ( 'NONE', #7830, #13276, #3826, .T. ) ;
#7875=ORIENTED_EDGE ( 'NONE', *, *, #338, .F. ) ;
#7899=VERTEX_POINT ( 'NONE', #6554 ) ;
#7929=CYLINDRICAL_SURFACE ( 'NONE', #12271, 2.500000000000000444 ) ;
#7935=CARTESIAN_POINT ( 'NONE',  ( 0.3126073911696399255, 2.020725942163686728, -3.499999999999999556 ) ) ;
#7986=DIRECTION ( 'NONE',  ( -1.000000000000000000, -0.000000000000000000, -0.000000000000000000 ) ) ;
#8047=CARTESIAN_POINT ( 'NONE',  ( 4.158806752148102248, -2.089318365061878069, 3.500000000000000000 ) ) ;
#8067=CARTESIAN_POINT ( 'NONE',  ( 3.958484000407173298, -3.734437307742043632, -0.5317648453100631833 ) ) ;
#8087=B_SPLINE_CURVE_WITH_KNOTS ( 'NONE', 3,
 ( #14795, #16180, #2790, #11771 ),
 .UNSPECIFIED., .F., .F.,
 ( 4, 4 ),
 ( 0.002080789711329297104, 0.004173039763574517766 ),
 .UNSPECIFIED. ) ;
#8099=ORIENTED_EDGE ( 'NONE', *, *, #16055, .T. ) ;
#8113=ORIENTED_EDGE ( 'NONE', *, *, #13406, .F. ) ;
#8121=ORIENTED_EDGE ( 'NONE', *, *, #4980, .T. ) ;
#8124=ORIENTED_EDGE ( 'NONE', *, *, #15182, .F. ) ;
#8125=B_SPLINE_CURVE_WITH_KNOTS ( 'NONE', 3,
 ( #5630, #1037, #1225, #17447, #4058 ),
 .UNSPECIFIED., .F., .F.,
 ( 4, 1, 4 ),
 ( 0.000000000000000000, 0.002020725942163688338, 0.004041451884327376676 ),
 .UNSPECIFIED. ) ;
#8137=ORIENTED_EDGE ( 'NONE', *, *, #12958, .T. ) ;
#8140=DIRECTION ( 'NONE',  ( 0.000000000000000000, 0.000000000000000000, 1.000000000000000000 ) ) ;
#8157=B_SPLINE_CURVE_WITH_KNOTS ( 'NONE', 3,
 ( #16974, #1241, #8372, #11685, #18837, #7193 ),
 .UNSPECIFIED., .F., .F.,
 ( 4, 2, 4 ),
 ( 0.003805861006858102854, 0.004828937052660004989, 0.005852013098461907557 ),
 .UNSPECIFIED. ) ;
#8205=EDGE_CURVE ( 'NONE', #3020, #2658, #16781, .T. ) ;
#8222=CARTESIAN_POINT ( 'NONE',  ( 3.951447005078451813, 3.704664227300101143, 0.5833333333333334814 ) ) ;
#8231=CARTESIAN_POINT ( 'NONE',  ( 0.3126073911696399255, 2.020725942163686728, -3.499999999999999556 ) ) ;
#8244=CARTESIAN_POINT ( 'NONE',  ( 4.086376210449952140, 2.103254844323303008, 3.500000000000000000 ) ) ;
#8251=CARTESIAN_POINT ( 'NONE',  ( 3.973110223767137850, 2.263313079739336463E-11, 3.565797985667434222 ) ) ;
#8255=CARTESIAN_POINT ( 'NONE',  ( 25.60000000000000142, 0.000000000000000000, 2.055000000000000160 ) ) ;
#8286=ORIENTED_EDGE ( 'NONE', *, *, #5566, .F. ) ;
#8288=CARTESIAN_POINT ( 'NONE',  ( 3.973110223767137850, -2.261515145575163828E-11, -3.565797985667433778 ) ) ;
#8334=ORIENTED_EDGE ( 'NONE', *, *, #3381, .F. ) ;
#8336=CARTESIAN_POINT ( 'NONE',  ( 4.055498735588686010, -1.410041617599707475, 3.568038744583201805 ) ) ;
#8364=DIRECTION ( 'NONE',  ( 1.000000000000000000, 0.000000000000000000, -0.000000000000000000 ) ) ;
#8372=CARTESIAN_POINT ( 'NONE',  ( 0.1381419387119174058, -1.355287006778759684, 3.500000000000000888 ) ) ;
#8383=VERTEX_POINT ( 'NONE', #7097 ) ;
#8407=CARTESIAN_POINT ( 'NONE',  ( 4.158806965674310518, -4.075748668183989842, -0.05940377217584014852 ) ) ;
#8412=CARTESIAN_POINT ( 'NONE',  ( 1.562775787684183633E-16, 0.3423821193476820346, 3.500000000000000000 ) ) ;
#8453=CYLINDRICAL_SURFACE ( 'NONE', #5494, 2.500000000000000444 ) ;
#8481=CIRCLE ( 'NONE', #5696, 3.500000000000000000 ) ;
#8489=( NAMED_UNIT ( * ) SI_UNIT ( $, .STERADIAN. ) SOLID_ANGLE_UNIT ( ) );
#8501=CARTESIAN_POINT ( 'NONE',  ( 5.599999999999999645, -2.020725942163695166, -3.500000000000000000 ) ) ;
#8503=EDGE_CURVE ( 'NONE', #1391, #15492, #2895, .T. ) ;
#8506=LINE ( 'NONE', #14275, #18355 ) ;
#8511=CIRCLE ( 'NONE', #114, 2.500000000000000444 ) ;
#8515=B_SPLINE_CURVE_WITH_KNOTS ( 'NONE', 3,
 ( #18682, #17404, #17209, #14172, #15553, #3722, #9783, #14360, #14076, #9980, #5106, #6863, #15933, #2536, #9880, #15649 ),
 .UNSPECIFIED., .F., .F.,
 ( 4, 3, 3, 3, 3, 4 ),
 ( 0.000000000000000000, 3.315506744709606176E-05, 6.608280158701084731E-05, 0.0001026520855292453537, 0.0001376952025668689477, 0.0001398064759194506818 ),
 .UNSPECIFIED. ) ;
#8524=B_SPLINE_CURVE_WITH_KNOTS ( 'NONE', 3,
 ( #13474, #307, #6159, #6445, #4987 ),
 .UNSPECIFIED., .F., .F.,
 ( 4, 1, 4 ),
 ( 0.000000000000000000, 0.002020725942163692675, 0.004041451884327385349 ),
 .UNSPECIFIED. ) ;
#8547=DIRECTION ( 'NONE',  ( 0.000000000000000000, 0.000000000000000000, 1.000000000000000000 ) ) ;
#8551=CARTESIAN_POINT ( 'NONE',  ( 3.974175853610046438, 3.450041667725685102, -1.156004144283996116 ) ) ;
#8561=EDGE_LOOP ( 'NONE', ( #13306, #8906, #2932, #15688 ) ) ;
#8596=CARTESIAN_POINT ( 'NONE',  ( 4.050536630291688311, 2.401306687817038821, -2.976670123173768001 ) ) ;
#8666=EDGE_LOOP ( 'NONE', ( #1606, #14813, #5814, #6254, #18545 ) ) ;
#8697=CIRCLE ( 'NONE', #18650, 3.500000000000000000 ) ;
#8703=CARTESIAN_POINT ( 'NONE',  ( 0.000000000000000000, 3.755786496842902015E-16, 3.500000000000000000 ) ) ;
#8719=VERTEX_POINT ( 'NONE', #995 ) ;
#8744=ADVANCED_FACE ( 'NONE', ( #11341 ), #12832, .F. ) ;
#8752=DIRECTION ( 'NONE',  ( 0.000000000000000000, 0.000000000000000000, -1.000000000000000000 ) ) ;
#8766=EDGE_CURVE ( 'NONE', #3532, #13429, #8511, .T. ) ;
#8767=CARTESIAN_POINT ( 'NONE',  ( 0.02944718078427176200, -0.6813962075686350595, -3.500000000000000000 ) ) ;
#8794=FACE_OUTER_BOUND ( 'NONE', #5555, .T. ) ;
#8811=LINE ( 'NONE', #332, #15529 ) ;
#8831=ORIENTED_EDGE ( 'NONE', *, *, #1956, .T. ) ;
#8832=CARTESIAN_POINT ( 'NONE',  ( 0.3126073911696408136, 2.020725942163688060, 3.500000000000000000 ) ) ;
#8899=AXIS2_PLACEMENT_3D ( 'NONE', #6712, #8364, #18532 ) ;
#8906=ORIENTED_EDGE ( 'NONE', *, *, #13406, .T. ) ;
#8923=ORIENTED_EDGE ( 'NONE', *, *, #17119, .T. ) ;
#8951=EDGE_LOOP ( 'NONE', ( #326, #5297, #18293, #5835, #8124 ) ) ;
#8953=CARTESIAN_POINT ( 'NONE',  ( 3.974167765203684866, 0.7238254970431302615, -3.565825589389262085 ) ) ;
#8982=CARTESIAN_POINT ( 'NONE',  ( 4.114405500665264448, -4.051151509359423031, 2.300149018892232304E-16 ) ) ;
#8987=EDGE_CURVE ( 'NONE', #3780, #5083, #8524, .T. ) ;
#8994=CONICAL_SURFACE ( 'NONE', #11493, 3.500000000000000000, 1.047197551196600296 ) ;
#9009=ORIENTED_EDGE ( 'NONE', *, *, #3990, .F. ) ;
#9035=EDGE_CURVE ( 'NONE', #8383, #5869, #3850, .T. ) ;
#9053=CARTESIAN_POINT ( 'NONE',  ( 3.880198502136737115, 0.7307680362927179152, -3.499999999999999556 ) ) ;
#9074=CARTESIAN_POINT ( 'NONE',  ( 4.142654963991909689, 2.035398498734317219, -3.525413613457259565 ) ) ;
#9083=B_SPLINE_CURVE_WITH_KNOTS ( 'NONE', 3,
 ( #18740, #5459, #11401, #17462 ),
 .UNSPECIFIED., .F., .F.,
 ( 4, 4 ),
 ( 2.380739282167635349E-07, 0.002044882221487541018 ),
 .UNSPECIFIED. ) ;
#9084=DIRECTION ( 'NONE',  ( 0.000000000000000000, -1.073081856240827827E-16, 1.000000000000000000 ) ) ;
#9112=EDGE_CURVE ( 'NONE', #10812, #11132, #10602, .T. ) ;
#9125=AXIS2_PLACEMENT_3D ( 'NONE', #7082, #17739, #2391 ) ;
#9146=DIRECTION ( 'NONE',  ( -1.000000000000000000, -0.000000000000000000, -0.000000000000000000 ) ) ;
#9157=CARTESIAN_POINT ( 'NONE',  ( 0.000000000000000000, 3.755786496842902015E-16, 3.500000000000000000 ) ) ;
#9170=ORIENTED_EDGE ( 'NONE', *, *, #17119, .F. ) ;
#9171=CARTESIAN_POINT ( 'NONE',  ( 4.175075985190094485, 2.060370777630109007, -3.568666869285570531 ) ) ;
#9173=CARTESIAN_POINT ( 'NONE',  ( 4.124214193018028496, -4.056676826581953499, 2.739218076410093718E-16 ) ) ;
#9174=ORIENTED_EDGE ( 'NONE', *, *, #2418, .T. ) ;
#9189=CARTESIAN_POINT ( 'NONE',  ( 4.175326769692873086, 4.121399112977848667, 2.543528568011644531E-14 ) ) ;
#9193=DIRECTION ( 'NONE',  ( -1.000000000000000000, -0.000000000000000000, -0.000000000000000000 ) ) ;
#9242=DIRECTION ( 'NONE',  ( 0.000000000000000000, 1.000000000000000000, -1.073081856240829182E-16 ) ) ;
#9259=ADVANCED_FACE ( 'NONE', ( #13697 ), #7929, .T. ) ;
#9280=CARTESIAN_POINT ( 'NONE',  ( 4.052424581287662697, 3.786734753435040179, 0.5771415817957487038 ) ) ;
#9285=CARTESIAN_POINT ( 'NONE',  ( 4.165266963751924401, 4.099263933823841910, -9.393296756667078455E-16 ) ) ;
#9304=DIRECTION ( 'NONE',  ( 1.000000000000000000, 0.000000000000000000, -0.000000000000000000 ) ) ;
#9327=ORIENTED_EDGE ( 'NONE', *, *, #3012, .F. ) ;
#9329=LINE ( 'NONE', #10705, #12097 ) ;
#9346=CARTESIAN_POINT ( 'NONE',  ( 5.599999999999999645, 4.041451884327382338, 0.000000000000000000 ) ) ;
#9381=DIRECTION ( 'NONE',  ( 0.000000000000000000, 0.000000000000000000, -1.000000000000000000 ) ) ;
#9382=UNCERTAINTY_MEASURE_WITH_UNIT (LENGTH_MEASURE( 1.000000000000000082E-05 ), #7132, 'distance_accuracy_value', 'NONE');
#9387=VERTEX_POINT ( 'NONE', #5497 ) ;
#9428=DIRECTION ( 'NONE',  ( 0.000000000000000000, -1.000000000000000000, 0.000000000000000000 ) ) ;
#9429=AXIS2_PLACEMENT_3D ( 'NONE', #10459, #1388, #10365 ) ;
#9449=CARTESIAN_POINT ( 'NONE',  ( 4.082498951862916670, 2.020725942163688504, 3.500000000000000000 ) ) ;
#9460=CARTESIAN_POINT ( 'NONE',  ( 4.151274195509476073, 2.039912954708820170, -3.533232880573633050 ) ) ;
#9463=ORIENTED_EDGE ( 'NONE', *, *, #4373, .F. ) ;
#9479=CARTESIAN_POINT ( 'NONE',  ( 4.114405500665261783, 4.051151509359415925, -1.111238067874716415E-16 ) ) ;
#9484=ORIENTED_EDGE ( 'NONE', *, *, #19165, .T. ) ;
#9498=CARTESIAN_POINT ( 'NONE',  ( 3.951447005078451813, -1.347150628109132553, -3.500000000000000444 ) ) ;
#9514=CARTESIAN_POINT ( 'NONE',  ( 4.050536630291690976, 3.778525289263159781, 0.5912575323401411120 ) ) ;
#9528=CARTESIAN_POINT ( 'NONE',  ( 3.974175853610028231, -2.726149789692840386, -2.409821656223227748 ) ) ;
#9569=EDGE_LOOP ( 'NONE', ( #13477, #16342 ) ) ;
#9591=CARTESIAN_POINT ( 'NONE',  ( 3.973514160553464514, -3.435084588004195805, 1.181876024140317227 ) ) ;
#9634=SHAPE_REPRESENTATION ( 'hex flange bolt small_iso_ISO 4162 - M5 x 20 x 20-N', ( #10540 ), #19229 ) ;
#9684=CARTESIAN_POINT ( 'NONE',  ( 4.071447262713887127, 2.020725942163688504, 3.500000000000000000 ) ) ;
#9685=ORIENTED_EDGE ( 'NONE', *, *, #11911, .T. ) ;
#9695=CARTESIAN_POINT ( 'NONE',  ( 0.000000000000000000, 3.755786496842896592E-16, -3.499999999999999556 ) ) ;
#9700=ORIENTED_EDGE ( 'NONE', *, *, #6792, .F. ) ;
#9748=DIRECTION ( 'NONE',  ( -1.000000000000000000, -0.000000000000000000, -0.000000000000000000 ) ) ;
#9783=CARTESIAN_POINT ( 'NONE',  ( 4.132952817037867987, -2.031684012687262175, 3.518979934899752138 ) ) ;
#9804=ORIENTED_EDGE ( 'NONE', *, *, #16632, .F. ) ;
#9811=B_SPLINE_CURVE_WITH_KNOTS ( 'NONE', 3,
 ( #1490, #4615, #7731, #7444 ),
 .UNSPECIFIED., .F., .F.,
 ( 4, 4 ),
 ( 0.002080789711329271950, 0.004173039763574512562 ),
 .UNSPECIFIED. ) ;
#9825=DIRECTION ( 'NONE',  ( 1.000000000000000000, 0.000000000000000000, 0.000000000000000000 ) ) ;
#9826=EDGE_LOOP ( 'NONE', ( #8113, #16896, #19121, #12200 ) ) ;
#9830=FACE_OUTER_BOUND ( 'NONE', #4776, .T. ) ;
#9833=CARTESIAN_POINT ( 'NONE',  ( 3.880206590543030298, 3.396506438958510898, -1.117078279489021053 ) ) ;
#9880=CARTESIAN_POINT ( 'NONE',  ( 4.175572532730931208, -2.061029303918050282, 3.569807470274392713 ) ) ;
#9900=DIRECTION ( 'NONE',  ( 0.000000000000000000, 0.000000000000000000, -1.000000000000000000 ) ) ;
#9927=CARTESIAN_POINT ( 'NONE',  ( 4.071447262713887127, -2.020725942163688060, 3.500000000000000444 ) ) ;
#9933=CARTESIAN_POINT ( 'NONE',  ( 3.948103430091329358, 2.682758828852234156, -2.353325403974033669 ) ) ;
#9952=CARTESIAN_POINT ( 'NONE',  ( 3.951447005078455366, -3.704664227300106916, -0.5833333333333337034 ) ) ;
#9956=ORIENTED_EDGE ( 'NONE', *, *, #4577, .F. ) ;
#9980=CARTESIAN_POINT ( 'NONE',  ( 4.158413352280814657, -2.044871626972826650, 3.541821552872969292 ) ) ;
#9990=CARTESIAN_POINT ( 'NONE',  ( 4.180231891692618440, 2.049421325483208101, 3.591231015387272851 ) ) ;
#10005=CARTESIAN_POINT ( 'NONE',  ( 0.3126073911696428675, 4.041451884327382338, -3.240528425403984455E-16 ) ) ;
#10029=B_SPLINE_CURVE_WITH_KNOTS ( 'NONE', 3,
 ( #3488, #9449, #15414, #13942, #581, #16976, #15711, #15899, #12962, #18933, #6830, #17176, #3779, #18642, #11305, #3976 ),
 .UNSPECIFIED., .F., .F.,
 ( 4, 3, 3, 3, 3, 4 ),
 ( 0.000000000000000000, 3.315506744709148100E-05, 6.608280158700110304E-05, 0.0001026520855292349047, 0.0001376952025668703029, 0.0001398064759194511696 ),
 .UNSPECIFIED. ) ;
#10107=CARTESIAN_POINT ( 'NONE',  ( 0.3126073911696462537, -4.041451884327388555, -1.676097590879904329E-16 ) ) ;
#10109=ADVANCED_FACE ( 'NONE', ( #18149 ), #12375, .F. ) ;
#10153=LINE ( 'NONE', #2619, #10824 ) ;
#10162=VERTEX_POINT ( 'NONE', #3387 ) ;
#10219=CARTESIAN_POINT ( 'NONE',  ( 4.086262629614029862, 4.082406995609984435, 0.07093633357110337712 ) ) ;
#10230=ADVANCED_FACE ( 'NONE', ( #2400, #9830 ), #567, .T. ) ;
#10323=DIRECTION ( 'NONE',  ( 1.000000000000000000, 0.000000000000000000, -0.000000000000000000 ) ) ;
#10365=DIRECTION ( 'NONE',  ( 0.000000000000000000, 0.000000000000000000, -1.000000000000000000 ) ) ;
#10404=CARTESIAN_POINT ( 'NONE',  ( 0.000000000000000000, 0.000000000000000000, 0.000000000000000000 ) ) ;
#10419=CARTESIAN_POINT ( 'NONE',  ( 4.175813232069148562, -2.061359961916374495, -3.570380186727398097 ) ) ;
#10438=ADVANCED_FACE ( 'NONE', ( #16368 ), #8453, .T. ) ;
#10450=CARTESIAN_POINT ( 'NONE',  ( 4.175572532730935649, -4.122058607836119215, -1.475653861719983332E-15 ) ) ;
#10451=ORIENTED_EDGE ( 'NONE', *, *, #15263, .F. ) ;
#10459=CARTESIAN_POINT ( 'NONE',  ( 0.000000000000000000, 0.000000000000000000, 0.000000000000000000 ) ) ;
#10481=CARTESIAN_POINT ( 'NONE',  ( 5.100000000000002309, 6.368163355566238354E-16, -5.200000000000001066 ) ) ;
#10523=CARTESIAN_POINT ( 'NONE',  ( 4.033895293471413623, 1.419609371826631827, -3.499999999999999112 ) ) ;
#10540=AXIS2_PLACEMENT_3D ( 'NONE', #7341, #19270, #11738 ) ;
#10541=EDGE_CURVE ( 'NONE', #10812, #7830, #13278, .T. ) ;
#10550=CARTESIAN_POINT ( 'NONE',  ( 4.114405500665267112, 2.025575754679705298, -3.508400121684926987 ) ) ;
#10562=CARTESIAN_POINT ( 'NONE',  ( 3.950241966888465406, 2.668221755853712907, 2.378504353001160254 ) ) ;
#10566=ORIENTED_EDGE ( 'NONE', *, *, #3342, .T. ) ;
#10568=LINE ( 'NONE', #1679, #15838 ) ;
#10602=B_SPLINE_CURVE_WITH_KNOTS ( 'NONE', 3,
 ( #1400, #140, #7353, #16440, #1308, #6090 ),
 .UNSPECIFIED., .F., .F.,
 ( 4, 2, 4 ),
 ( 0.002044882221487541018, 0.003063384235218501520, 0.004081886248949461587 ),
 .UNSPECIFIED. ) ;
#10613=LINE ( 'NONE', #7778, #3655 ) ;
#10657=DIRECTION ( 'NONE',  ( 0.000000000000000000, 0.000000000000000000, 1.000000000000000000 ) ) ;
#10702=AXIS2_PLACEMENT_3D ( 'NONE', #2061, #9193, #13786 ) ;
#10705=CARTESIAN_POINT ( 'NONE',  ( 4.630153689607048761, 6.577590292450083844E-16, 5.371010071662833063 ) ) ;
#10724=DIRECTION ( 'NONE',  ( -0.000000000000000000, 0.000000000000000000, -1.000000000000000000 ) ) ;
#10751=VERTEX_POINT ( 'NONE', #10808 ) ;
#10753=CARTESIAN_POINT ( 'NONE',  ( 4.124214193018025831, 4.056676826581947282, -1.560956519390234888E-16 ) ) ;
#10771=AXIS2_PLACEMENT_3D ( 'NONE', #16678, #3284, #9242 ) ;
#10797=ORIENTED_EDGE ( 'NONE', *, *, #1001, .F. ) ;
#10799=CARTESIAN_POINT ( 'NONE',  ( 3.972066048304760955, -3.435565134476476601, -1.180968096049750393 ) ) ;
#10808=CARTESIAN_POINT ( 'NONE',  ( 0.3126073911695752550, -2.020725942163798194, -3.500000000000000000 ) ) ;
#10812=VERTEX_POINT ( 'NONE', #16773 ) ;
#10817=CARTESIAN_POINT ( 'NONE',  ( 4.630153689607048761, 0.000000000000000000, 0.000000000000000000 ) ) ;
#10824=VECTOR ( 'NONE', #11709, 1000.000000000000000 ) ;
#10842=CARTESIAN_POINT ( 'NONE',  ( 3.958484000407190617, 3.734437307742054735, 0.5317648453100325412 ) ) ;
#10871=ORIENTED_EDGE ( 'NONE', *, *, #17157, .T. ) ;
#10882=ADVANCED_BREP_SHAPE_REPRESENTATION ( '', ( #1125, #10540 ), #19229 ) ;
#10918=DIRECTION ( 'NONE',  ( -0.000000000000000000, 0.000000000000000000, 1.000000000000000000 ) ) ;
#10927=ORIENTED_EDGE ( 'NONE', *, *, #13066, .F. ) ;
#10947=CARTESIAN_POINT ( 'NONE',  ( 0.000000000000000000, -3.031088913245533867, -1.750000000000002220 ) ) ;
#10962=CARTESIAN_POINT ( 'NONE',  ( 3.806834918298644066, -4.336808689942017736E-15, -3.500000000000000000 ) ) ;
#10974=CARTESIAN_POINT ( 'NONE',  ( 3.972709601346592123, 3.429395227388311707, 1.191688283765306000 ) ) ;
#10986=ADVANCED_FACE ( 'NONE', ( #4259 ), #5449, .F. ) ;
#10989=CARTESIAN_POINT ( 'NONE',  ( 3.878096787214418306, -3.381939201670154826, -1.142309474598376395 ) ) ;
#11025=EDGE_LOOP ( 'NONE', ( #15341, #2682, #5190, #2973, #3533 ) ) ;
#11041=CARTESIAN_POINT ( 'NONE',  ( 4.142654963991903472, 4.070796997468637102, -1.539416769003468026E-16 ) ) ;
#11078=CARTESIAN_POINT ( 'NONE',  ( 3.973110223768738791, 0.6864646529411682074, 3.565797985667475967 ) ) ;
#11112=MECHANICAL_DESIGN_GEOMETRIC_PRESENTATION_REPRESENTATION('',(#17992),#15486);
#11132=VERTEX_POINT ( 'NONE', #17751 ) ;
#11138=DIRECTION ( 'NONE',  ( 1.000000000000000000, 0.000000000000000000, 0.000000000000000000 ) ) ;
#11142=CARTESIAN_POINT ( 'NONE',  ( 3.961551342854190860, -3.742715940867773927, 0.5174258321190744470 ) ) ;
#11143=EDGE_CURVE ( 'NONE', #7830, #18099, #856, .T. ) ;
#11166=B_SPLINE_CURVE_WITH_KNOTS ( 'NONE', 3,
 ( #17604, #17511, #6964, #11734, #14462, #15857 ),
 .UNSPECIFIED., .F., .F.,
 ( 4, 2, 4 ),
 ( 0.002044882221487525839, 0.003063384235218491979, 0.004081886248949458118 ),
 .UNSPECIFIED. ) ;
#11172=CARTESIAN_POINT ( 'NONE',  ( 3.972058292797709278, 0.6948821373597366957, 3.565770528409240470 ) ) ;
#11173=CIRCLE ( 'NONE', #5882, 2.500000000000000444 ) ;
#11214=SHAPE_DEFINITION_REPRESENTATION ( #3575, #9634 ) ;
#11249=CARTESIAN_POINT ( 'NONE',  ( 4.050536630291690976, -2.401306687817041929, 2.976670123173769333 ) ) ;
#11288=FACE_OUTER_BOUND ( 'NONE', #15554, .T. ) ;
#11297=CARTESIAN_POINT ( 'NONE',  ( 4.180231891692620216, 4.134807952925571684, 0.02076457676760292553 ) ) ;
#11305=CARTESIAN_POINT ( 'NONE',  ( 4.175572532730931208, 2.061029303918050726, 3.569807470274392713 ) ) ;
#11307=CONICAL_SURFACE ( 'NONE', #13796, 3.500000000000000000, 1.047197551196600296 ) ;
#11341=FACE_OUTER_BOUND ( 'NONE', #13224, .T. ) ;
#11388=PRODUCT ( 'hex flange bolt small_iso_ISO 4162 - M5 x 20 x 20-N', 'hex flange bolt small_iso_ISO 4162 - M5 x 20 x 20-N', '', ( #14045 ) ) ;
#11395=CARTESIAN_POINT ( 'NONE',  ( 4.033901012035826739, 3.740908793663638487, -0.5205559028932524868 ) ) ;
#11399=DIRECTION ( 'NONE',  ( 1.000000000000000000, 0.000000000000000000, 0.000000000000000000 ) ) ;
#11401=CARTESIAN_POINT ( 'NONE',  ( -6.468631247035699870E-16, -3.375361811986504534, 1.153701847711635198 ) ) ;
#11406=VERTEX_POINT ( 'NONE', #1214 ) ;
#11414=ORIENTED_EDGE ( 'NONE', *, *, #3381, .T. ) ;
#11438=ORIENTED_EDGE ( 'NONE', *, *, #18097, .F. ) ;
#11493=AXIS2_PLACEMENT_3D ( 'NONE', #13133, #5635, #4444 ) ;
#11509=DIRECTION ( 'NONE',  ( -1.000000000000000000, -0.000000000000000000, -0.000000000000000000 ) ) ;
#11538=CARTESIAN_POINT ( 'NONE',  ( 4.175813232069146785, 2.061359961916366057, -3.570380186727397653 ) ) ;
#11542=CARTESIAN_POINT ( 'NONE',  ( 0.2182387239031248483, 1.693823289467350390, 3.500000000000000000 ) ) ;
#11549=CARTESIAN_POINT ( 'NONE',  ( 5.599999999999999645, 0.000000000000000000, 0.000000000000000000 ) ) ;
#11629=( GEOMETRIC_REPRESENTATION_CONTEXT ( 3 ) GLOBAL_UNCERTAINTY_ASSIGNED_CONTEXT ( ( #17216 ) ) GLOBAL_UNIT_ASSIGNED_CONTEXT ( ( #16424, #17896, #16813 ) ) REPRESENTATION_CONTEXT ( 'NONE', 'WORKASPACE' ) );
#11663=DIRECTION ( 'NONE',  ( 0.000000000000000000, -1.000000000000000000, -1.073081856240827827E-16 ) ) ;
#11675=EDGE_LOOP ( 'NONE', ( #330, #12342, #8137, #17972, #9463 ) ) ;
#11685=CARTESIAN_POINT ( 'NONE',  ( 0.02944718078426969768, -0.6813962075686098574, 3.500000000000000888 ) ) ;
#11709=DIRECTION ( 'NONE',  ( -1.000000000000000000, -0.000000000000000000, -0.000000000000000000 ) ) ;
#11714=B_SPLINE_CURVE_WITH_KNOTS ( 'NONE', 3,
 ( #7729, #12221, #3428, #5097, #9479, #10753, #3230, #11041, #15442, #420, #9285, #18384, #6461, #9189, #15545, #2054 ),
 .UNSPECIFIED., .F., .F.,
 ( 4, 3, 3, 3, 3, 4 ),
 ( 0.000000000000000000, 3.315506744709139969E-05, 6.608280158700174001E-05, 0.0001026520855292366530, 0.0001376952025668715498, 0.0001398064759194521725 ),
 .UNSPECIFIED. ) ;
#11734=CARTESIAN_POINT ( 'NONE',  ( 0.1388410611046087539, 3.710337782248032568, 0.5735064479039790886 ) ) ;
#11738=DIRECTION ( 'NONE',  ( 1.000000000000000000, 0.000000000000000000, 0.000000000000000000 ) ) ;
#11770=AXIS2_PLACEMENT_3D ( 'NONE', #13087, #15929, #5489 ) ;
#11771=CARTESIAN_POINT ( 'NONE',  ( 4.175813232069146785, 2.061359961916366057, -3.570380186727397653 ) ) ;
#11827=B_SPLINE_CURVE_WITH_KNOTS ( 'NONE', 3,
 ( #18414, #9514, #10974, #12354, #15480, #2282 ),
 .UNSPECIFIED., .F., .F.,
 ( 4, 2, 4 ),
 ( 0.000000000000000000, 0.002086519881787259317, 0.004173039763574518633 ),
 .UNSPECIFIED. ) ;
#11832=FACE_OUTER_BOUND ( 'NONE', #3581, .T. ) ;
#11837=DIRECTION ( 'NONE',  ( -0.7071067811865505703, 8.659560562354895880E-17, -0.7071067811865444641 ) ) ;
#11877=DIRECTION ( 'NONE',  ( 1.000000000000000000, 0.000000000000000000, 0.000000000000000000 ) ) ;
#11889=CARTESIAN_POINT ( 'NONE',  ( 4.158807179406255550, 2.089320655794525639, -3.500000000000000000 ) ) ;
#11911=EDGE_CURVE ( 'NONE', #18754, #14350, #6759, .T. ) ;
#11931=DIRECTION ( 'NONE',  ( -1.000000000000000000, -0.000000000000000000, -0.000000000000000000 ) ) ;
#12012=VERTEX_POINT ( 'NONE', #3369 ) ;
#12060=B_SPLINE_CURVE_WITH_KNOTS ( 'NONE', 3,
 ( #12525, #12726, #10962, #9498, #18496 ),
 .UNSPECIFIED., .F., .F.,
 ( 4, 1, 4 ),
 ( 0.000000000000000000, 0.002020725942163690940, 0.004041451884327381880 ),
 .UNSPECIFIED. ) ;
#12067=AXIS2_PLACEMENT_3D ( 'NONE', #16061, #9084, #11663 ) ;
#12097=VECTOR ( 'NONE', #12553, 1000.000000000000114 ) ;
#12111=CARTESIAN_POINT ( 'NONE',  ( 4.151274195509471632, -4.079825909417648333, 5.067843131179045271E-16 ) ) ;
#12116=AXIS2_PLACEMENT_3D ( 'NONE', #10481, #7455, #523 ) ;
#12122=EDGE_CURVE ( 'NONE', #1594, #7899, #7699, .T. ) ;
#12124=CARTESIAN_POINT ( 'NONE',  ( 3.974175853610081077, 2.726149789692974945, 2.409821656223290365 ) ) ;
#12149=ORIENTED_EDGE ( 'NONE', *, *, #6792, .T. ) ;
#12151=EDGE_CURVE ( 'NONE', #2374, #8719, #13996, .T. ) ;
#12177=LINE ( 'NONE', #1818, #6193 ) ;
#12200=ORIENTED_EDGE ( 'NONE', *, *, #15121, .F. ) ;
#12204=CARTESIAN_POINT ( 'NONE',  ( 4.165266963751926177, -4.099263933823847239, 5.067843131179045271E-16 ) ) ;
#12221=CARTESIAN_POINT ( 'NONE',  ( 4.082498951862917558, 4.041451884327382338, 2.013392555975283473E-32 ) ) ;
#12241=CARTESIAN_POINT ( 'NONE',  ( 0.000000000000000000, 0.000000000000000000, 0.000000000000000000 ) ) ;
#12243=VECTOR ( 'NONE', #9748, 1000.000000000000000 ) ;
#12264=CARTESIAN_POINT ( 'NONE',  ( 4.050880675075949178, 1.379097446046194220, 3.567934390854430760 ) ) ;
#12271=AXIS2_PLACEMENT_3D ( 'NONE', #13880, #7834, #519 ) ;
#12275=CARTESIAN_POINT ( 'NONE',  ( 4.132952817037860882, -2.031684012687265284, -3.518979934899746365 ) ) ;
#12304=PLANE ( 'NONE',  #82 ) ;
#12311=CARTESIAN_POINT ( 'NONE',  ( 0.000000000000000000, 0.000000000000000000, 0.000000000000000000 ) ) ;
#12340=EDGE_CURVE ( 'NONE', #104, #10751, #1288, .T. ) ;
#12342=ORIENTED_EDGE ( 'NONE', *, *, #4577, .T. ) ;
#12354=CARTESIAN_POINT ( 'NONE',  ( 3.973514160553461849, 2.741076955031360285, 2.383932505289870996 ) ) ;
#12375=PLANE ( 'NONE',  #10771 ) ;
#12376=EDGE_CURVE ( 'NONE', #17929, #3617, #2825, .T. ) ;
#12387=CARTESIAN_POINT ( 'NONE',  ( 25.60000000000000142, 0.000000000000000000, 0.000000000000000000 ) ) ;
#12389=CARTESIAN_POINT ( 'NONE',  ( 5.599999999999999645, 2.020725942163688504, 3.500000000000000000 ) ) ;
#12402=CONICAL_SURFACE ( 'NONE', #4611, 3.500000000000000000, 1.047197551196600296 ) ;
#12418=CARTESIAN_POINT ( 'NONE',  ( 0.3126073911695752550, -2.020725942163798194, -3.500000000000000000 ) ) ;
#12436=ORIENTED_EDGE ( 'NONE', *, *, #6388, .F. ) ;
#12470=ADVANCED_FACE ( 'NONE', ( #8794 ), #13097, .F. ) ;
#12519=CARTESIAN_POINT ( 'NONE',  ( 4.050823680195225762, -3.779313952391384568, 0.5899027668435158356 ) ) ;
#12525=CARTESIAN_POINT ( 'NONE',  ( 4.071447262713887127, 2.020725942163686728, -3.499999999999999556 ) ) ;
#12538=CARTESIAN_POINT ( 'NONE',  ( 0.02993401039713562001, 2.688325911136453250, -2.343682934607766111 ) ) ;
#12542=AXIS2_PLACEMENT_3D ( 'NONE', #18083, #1753, #400 ) ;
#12553=DIRECTION ( 'NONE',  ( 0.3420201433256622736, 1.150791560227853228E-16, 0.9396926207859106484 ) ) ;
#12610=CARTESIAN_POINT ( 'NONE',  ( 3.880206590543342493, -3.396506438958446061, 1.117078279489142512 ) ) ;
#12620=CARTESIAN_POINT ( 'NONE',  ( 0.2182387239031244319, 1.693823289467349724, -3.499999999999999556 ) ) ;
#12634=CARTESIAN_POINT ( 'NONE',  ( 0.000000000000000000, 3.031088913245532979, -1.750000000000004219 ) ) ;
#12667=CARTESIAN_POINT ( 'NONE',  ( 4.071447262713887127, 2.020725942163688504, 3.500000000000000000 ) ) ;
#12680=ORIENTED_EDGE ( 'NONE', *, *, #15182, .T. ) ;
#12709=CARTESIAN_POINT ( 'NONE',  ( 4.055492966679648426, -3.795017426214730705, 0.5629142681441111629 ) ) ;
#12726=CARTESIAN_POINT ( 'NONE',  ( 3.951447005078448260, 1.347150628109122561, -3.499999999999999112 ) ) ;
#12760=B_SPLINE_CURVE_WITH_KNOTS ( 'NONE', 3,
 ( #16584, #6328, #13190, #19160, #3188, #15301 ),
 .UNSPECIFIED., .F., .F.,
 ( 4, 2, 4 ),
 ( 1.316110421120630972E-19, 0.002086519881787259317, 0.004173039763574518633 ),
 .UNSPECIFIED. ) ;
#12805=DIRECTION ( 'NONE',  ( -1.000000000000000000, -0.000000000000000000, -0.000000000000000000 ) ) ;
#12807=CARTESIAN_POINT ( 'NONE',  ( 4.030867648406119663, -2.329326259789124443, 2.965488570641622523 ) ) ;
#12832=( BOUNDED_SURFACE ( )  B_SPLINE_SURFACE ( 3, 2, ( 
 ( #12904, #8407, #17403 ),
 ( #11142, #6764, #12709 ),
 ( #12610, #18871, #3812 ),
 ( #6862, #15648, #5493 ),
 ( #15841, #12807, #18680 ),
 ( #6951, #17208, #15932 ) ),
 .UNSPECIFIED., .F., .F., .F. ) 
 B_SPLINE_SURFACE_WITH_KNOTS ( ( 4, 2, 4 ),
 ( 3, 3 ),
 ( 0.01651999345535505592, 0.01858032176739835700, 0.02064065007944165808 ),
 ( 0.000000000000000000, 1.000000000000000000 ),
 .UNSPECIFIED. ) 
 GEOMETRIC_REPRESENTATION_ITEM ( )  RATIONAL_B_SPLINE_SURFACE ( (
 ( 1.000000000000000000, 0.8047781103519390244, 1.000000000000000000),
 ( 1.000000000000000000, 0.8123785825601840260, 1.000000000000000000),
 ( 1.000000000000000000, 0.8190671539791607447, 1.000000000000000000),
 ( 1.000000000000000000, 0.8192352254831567482, 1.000000000000000000),
 ( 1.000000000000000000, 0.8126129677214078972, 1.000000000000000000),
 ( 1.000000000000000000, 0.8047712537969722302, 1.000000000000000000) ) ) 
 REPRESENTATION_ITEM ( '' )  SURFACE ( )  );
#12834=CARTESIAN_POINT ( 'NONE',  ( 0.2174200650117532607, 2.185595227304857335, -3.214438021527932676 ) ) ;
#12898=B_SPLINE_CURVE_WITH_KNOTS ( 'NONE', 3,
 ( #9684, #16916, #17304, #8222, #2450 ),
 .UNSPECIFIED., .F., .F.,
 ( 4, 1, 4 ),
 ( 0.000000000000000000, 0.002020725942163690940, 0.004041451884327382747 ),
 .UNSPECIFIED. ) ;
#12904=CARTESIAN_POINT ( 'NONE',  ( 4.086262629614033415, -4.082406995609994205, -0.07093633357110862292 ) ) ;
#12909=DIRECTION ( 'NONE',  ( 0.000000000000000000, 0.5000000000000018874, 0.8660254037844375974 ) ) ;
#12958=EDGE_CURVE ( 'NONE', #3780, #18099, #6331, .T. ) ;
#12962=CARTESIAN_POINT ( 'NONE',  ( 4.151274195509468967, 2.039912954708818837, 3.533232880573625501 ) ) ;
#13000=ORIENTED_EDGE ( 'NONE', *, *, #8987, .F. ) ;
#13066=EDGE_CURVE ( 'NONE', #2658, #1546, #4911, .T. ) ;
#13087=CARTESIAN_POINT ( 'NONE',  ( 5.599999999999999645, 2.020725942163686728, -3.499999999999999556 ) ) ;
#13097=PLANE ( 'NONE',  #16428 ) ;
#13133=CARTESIAN_POINT ( 'NONE',  ( 0.000000000000000000, 0.000000000000000000, 0.000000000000000000 ) ) ;
#13170=CIRCLE ( 'NONE', #18792, 5.200000000000001066 ) ;
#13190=CARTESIAN_POINT ( 'NONE',  ( 3.972709601346594344, -3.429395227388318812, -1.191688283765307332 ) ) ;
#13224=EDGE_LOOP ( 'NONE', ( #1279, #13000, #7875, #1635 ) ) ;
#13276=VERTEX_POINT ( 'NONE', #6094 ) ;
#13278=CIRCLE ( 'NONE', #16399, 3.500000000000000000 ) ;
#13299=B_SPLINE_CURVE_WITH_KNOTS ( 'NONE', 3,
 ( #12418, #802, #18387, #10947 ),
 .UNSPECIFIED., .F., .F.,
 ( 4, 4 ),
 ( 2.380739282773697217E-07, 0.002044882221487522803 ),
 .UNSPECIFIED. ) ;
#13306=ORIENTED_EDGE ( 'NONE', *, *, #18097, .T. ) ;
#13331=CONICAL_SURFACE ( 'NONE', #1471, 3.500000000000000000, 1.047197551196600296 ) ;
#13394=( BOUNDED_SURFACE ( )  B_SPLINE_SURFACE ( 3, 2, ( 
 ( #3644, #11889, #2997 ),
 ( #4471, #10523, #3092 ),
 ( #9053, #16387, #8953 ),
 ( #15018, #1637, #17536 ),
 ( #14489, #6897, #14686 ),
 ( #7177, #14590, #7269 ) ),
 .UNSPECIFIED., .F., .F., .F. ) 
 B_SPLINE_SURFACE_WITH_KNOTS ( ( 4, 2, 4 ),
 ( 3, 3 ),
 ( 0.01652267773200353021, 0.01858309280828997212, 0.02064350788457641403 ),
 ( 0.000000000000000000, 1.000000000000000000 ),
 .UNSPECIFIED. ) 
 GEOMETRIC_REPRESENTATION_ITEM ( )  RATIONAL_B_SPLINE_SURFACE ( (
 ( 1.000000000000000000, 0.8047780975688292315, 1.000000000000000000),
 ( 1.000000000000000000, 0.8123789546324567956, 1.000000000000000000),
 ( 1.000000000000000000, 0.8190677982988761041, 1.000000000000000000),
 ( 1.000000000000000000, 0.8192346069552172150, 1.000000000000000000),
 ( 1.000000000000000000, 0.8126126759768910190, 1.000000000000000000),
 ( 1.000000000000000000, 0.8047712639312011307, 1.000000000000000000) ) ) 
 REPRESENTATION_ITEM ( '' )  SURFACE ( )  );
#13396=ORIENTED_EDGE ( 'NONE', *, *, #913, .F. ) ;
#13406=EDGE_CURVE ( 'NONE', #11406, #4621, #17731, .T. ) ;
#13425=DIRECTION ( 'NONE',  ( 0.000000000000000000, 0.000000000000000000, -1.000000000000000000 ) ) ;
#13429=VERTEX_POINT ( 'NONE', #13885 ) ;
#13439=FACE_OUTER_BOUND ( 'NONE', #18522, .T. ) ;
#13446=CARTESIAN_POINT ( 'NONE',  ( 4.151274195509469855, -2.039912954708825943, -3.533232880573625057 ) ) ;
#13474=CARTESIAN_POINT ( 'NONE',  ( 4.071447262713890680, -4.041451884327388555, 0.000000000000000000 ) ) ;
#13476=CARTESIAN_POINT ( 'NONE',  ( 4.132952817037863547, -4.063368025374529680, 2.739218076410093718E-16 ) ) ;
#13477=ORIENTED_EDGE ( 'NONE', *, *, #8503, .F. ) ;
#13492=CIRCLE ( 'NONE', #726, 2.055000000000000160 ) ;
#13531=DIRECTION ( 'NONE',  ( 0.000000000000000000, 0.000000000000000000, -1.000000000000000000 ) ) ;
#13533=VERTEX_POINT ( 'NONE', #8231 ) ;
#13536=DIRECTION ( 'NONE',  ( -0.7071067811865505703, 0.000000000000000000, 0.7071067811865444641 ) ) ;
#13565=CARTESIAN_POINT ( 'NONE',  ( 4.175813232069146785, 2.061359961916366057, -3.570380186727397653 ) ) ;
#13579=CARTESIAN_POINT ( 'NONE',  ( 4.158921614371309694, 4.076055977742305103, -0.05993604794450720780 ) ) ;
#13654=VECTOR ( 'NONE', #11509, 1000.000000000000000 ) ;
#13664=CARTESIAN_POINT ( 'NONE',  ( 4.071447262713887127, 2.020725942163686728, -3.499999999999999556 ) ) ;
#13675=AXIS2_PLACEMENT_3D ( 'NONE', #10817, #18541, #16784 ) ;
#13687=ORIENTED_EDGE ( 'NONE', *, *, #10541, .F. ) ;
#13697=FACE_OUTER_BOUND ( 'NONE', #1181, .T. ) ;
#13701=EDGE_CURVE ( 'NONE', #6061, #4621, #8506, .T. ) ;
#13711=CARTESIAN_POINT ( 'NONE',  ( 0.000000000000000000, 0.000000000000000000, 0.000000000000000000 ) ) ;
#13732=CARTESIAN_POINT ( 'NONE',  ( 4.071447262713888016, -2.020725942163695166, -3.500000000000000000 ) ) ;
#13734=DIRECTION ( 'NONE',  ( -1.000000000000000000, -0.000000000000000000, -0.000000000000000000 ) ) ;
#13735=ORIENTED_EDGE ( 'NONE', *, *, #17157, .F. ) ;
#13750=CARTESIAN_POINT ( 'NONE',  ( 25.60000000000000142, 0.000000000000000000, 0.000000000000000000 ) ) ;
#13762=FACE_OUTER_BOUND ( 'NONE', #9826, .T. ) ;
#13786=DIRECTION ( 'NONE',  ( 0.000000000000000000, 0.000000000000000000, 1.000000000000000000 ) ) ;
#13787=TOROIDAL_SURFACE ( 'NONE', #12542, 5.200000000000001066, 0.4999999999999978351 ) ;
#13796=AXIS2_PLACEMENT_3D ( 'NONE', #13711, #1611, #13425 ) ;
#13823=CARTESIAN_POINT ( 'NONE',  ( 4.175326769692872197, -2.060699556488933215, -3.569236330973462490 ) ) ;
#13853=CARTESIAN_POINT ( 'NONE',  ( 4.158413352280811104, -4.089743253945655077, 5.067843131179045271E-16 ) ) ;
#13875=B_SPLINE_CURVE_WITH_KNOTS ( 'NONE', 3,
 ( #11538, #8596, #7142, #1282, #1380, #4401 ),
 .UNSPECIFIED., .F., .F.,
 ( 4, 2, 4 ),
 ( 0.000000000000000000, 0.002086519881787259317, 0.004173039763574518633 ),
 .UNSPECIFIED. ) ;
#13880=CARTESIAN_POINT ( 'NONE',  ( 0.000000000000000000, 0.000000000000000000, 0.000000000000000000 ) ) ;
#13882=CARTESIAN_POINT ( 'NONE',  ( 4.175813232069147674, -2.061359961916367833, 3.570380186727398542 ) ) ;
#13885=CARTESIAN_POINT ( 'NONE',  ( 25.15499999999999758, 3.061616997868383634E-16, -2.500000000000000444 ) ) ;
#13920=CARTESIAN_POINT ( 'NONE',  ( 4.086262629614029862, -1.979770830881092625, -3.570936333571105070 ) ) ;
#13942=CARTESIAN_POINT ( 'NONE',  ( 4.104070371397480876, 2.023683613428366002, 3.505122836902507810 ) ) ;
#13943=ORIENTED_EDGE ( 'NONE', *, *, #9035, .T. ) ;
#13996=B_SPLINE_CURVE_WITH_KNOTS ( 'NONE', 3,
 ( #13882, #11249, #3629, #9591, #12519, #3537 ),
 .UNSPECIFIED., .F., .F.,
 ( 4, 2, 4 ),
 ( 0.000000000000000000, 0.002086519881787262786, 0.004173039763574524705 ),
 .UNSPECIFIED. ) ;
#14004=CARTESIAN_POINT ( 'NONE',  ( 4.180231680468789790, -2.085385483809537810, 3.570466434508605680 ) ) ;
#14045=PRODUCT_CONTEXT ( 'NONE', #6080, 'mechanical' ) ;
#14066=VERTEX_POINT ( 'NONE', #3968 ) ;
#14076=CARTESIAN_POINT ( 'NONE',  ( 4.151274195509476073, -2.039912954708822834, 3.533232880573632606 ) ) ;
#14145=ORIENTED_EDGE ( 'NONE', *, *, #7854, .T. ) ;
#14172=CARTESIAN_POINT ( 'NONE',  ( 4.104070371397485317, -2.023683613428366890, 3.505122836902509587 ) ) ;
#14195=CARTESIAN_POINT ( 'NONE',  ( 4.158921784487744411, 2.089935040870094074, 3.500000000000000444 ) ) ;
#14270=CONICAL_SURFACE ( 'NONE', #1791, 2.055000000000000160, 0.7853981633974439491 ) ;
#14275=CARTESIAN_POINT ( 'NONE',  ( 4.630153689607048761, 0.000000000000000000, -5.371010071662833063 ) ) ;
#14312=DIRECTION ( 'NONE',  ( 0.000000000000000000, 0.000000000000000000, -1.000000000000000000 ) ) ;
#14318=CARTESIAN_POINT ( 'NONE',  ( 4.158806965674307854, 4.075748668183980961, 0.05940377217583493047 ) ) ;
#14350=VERTEX_POINT ( 'NONE', #4806 ) ;
#14360=CARTESIAN_POINT ( 'NONE',  ( 4.142654963991909689, -2.035398498734318995, 3.525413613457260009 ) ) ;
#14406=DIRECTION ( 'NONE',  ( 1.000000000000000000, 0.000000000000000000, -0.000000000000000000 ) ) ;
#14408=ADVANCED_FACE ( 'NONE', ( #5713 ), #4145, .F. ) ;
#14444=SHAPE_REPRESENTATION_RELATIONSHIP ( 'NONE' , 'NONE' ,  #9634, #10882 ) ;
#14462=CARTESIAN_POINT ( 'NONE',  ( 0.2174200650117547873, 3.876582599186211731, 0.2855619784720684895 ) ) ;
#14489=CARTESIAN_POINT ( 'NONE',  ( 3.958476099524242731, -1.406653531810796443, -3.500000000000000000 ) ) ;
#14507=DIRECTION ( 'NONE',  ( 0.000000000000000000, 0.000000000000000000, -1.000000000000000000 ) ) ;
#14563=B_SPLINE_CURVE_WITH_KNOTS ( 'NONE', 3,
 ( #4495, #10450, #18969, #1184, #7520, #12204, #13853, #12111, #16608, #13476, #9173, #8982, #4797, #4888, #7808, #1850 ),
 .UNSPECIFIED., .F., .F.,
 ( 4, 3, 3, 3, 3, 4 ),
 ( -2.111273352579591097E-06, 0.000000000000000000, 3.519286887794390245E-05, 7.191842652046569998E-05, 0.0001049868727088885950, 0.0001382836236814613518 ),
 .UNSPECIFIED. ) ;
#14580=AXIS2_PLACEMENT_3D ( 'NONE', #17056, #9428, #15396 ) ;
#14590=CARTESIAN_POINT ( 'NONE',  ( 4.158921444904714271, -2.089933220600049157, -3.500000000000000000 ) ) ;
#14592=FACE_OUTER_BOUND ( 'NONE', #18654, .T. ) ;
#14605=CARTESIAN_POINT ( 'NONE',  ( 3.950241966887534151, 3.393956070637314859, -1.121495646999261186 ) ) ;
#14612=CARTESIAN_POINT ( 'NONE',  ( 0.000000000000000000, 0.000000000000000000, 0.000000000000000000 ) ) ;
#14686=CARTESIAN_POINT ( 'NONE',  ( 4.052416734886620908, -1.393505408945139301, -3.567979131523610459 ) ) ;
#14717=CARTESIAN_POINT ( 'NONE',  ( 0.3126073911695752550, -2.020725942163798194, -3.500000000000000000 ) ) ;
#14718=EDGE_CURVE ( 'NONE', #5869, #13533, #10153, .T. ) ;
#14751=CARTESIAN_POINT ( 'NONE',  ( 5.599999999999999645, -4.041451884327388555, 0.000000000000000000 ) ) ;
#14766=DIRECTION ( 'NONE',  ( -1.000000000000000000, -0.000000000000000000, -0.000000000000000000 ) ) ;
#14789=CARTESIAN_POINT ( 'NONE',  ( 0.000000000000000000, 3.031088913245533867, 1.750000000000002887 ) ) ;
#14795=CARTESIAN_POINT ( 'NONE',  ( 3.973110223767137850, -2.261515145575163828E-11, -3.565797985667433778 ) ) ;
#14813=ORIENTED_EDGE ( 'NONE', *, *, #1001, .T. ) ;
#14823=B_SPLINE_CURVE_WITH_KNOTS ( 'NONE', 3,
 ( #7935, #12620, #2359, #16837, #15753, #9695 ),
 .UNSPECIFIED., .F., .F.,
 ( 4, 2, 4 ),
 ( 0.01103795673506154963, 0.01206113197427181698, 0.01308430721348208606 ),
 .UNSPECIFIED. ) ;
#14888=ADVANCED_FACE ( 'NONE', ( #16309 ), #6144, .F. ) ;
#14931=CIRCLE ( 'NONE', #17746, 5.200000000000001066 ) ;
#14965=DIRECTION ( 'NONE',  ( 0.000000000000000000, 0.000000000000000000, -1.000000000000000000 ) ) ;
#14984=ADVANCED_FACE ( 'NONE', ( #4386 ), #4782, .F. ) ;
#15018=CARTESIAN_POINT ( 'NONE',  ( 3.878104551856474735, -0.7018542299754126912, -3.499999999999999556 ) ) ;
#15110=DIRECTION ( 'NONE',  ( 0.000000000000000000, 0.000000000000000000, 1.000000000000000000 ) ) ;
#15121=EDGE_CURVE ( 'NONE', #4621, #12012, #6789, .T. ) ;
#15122=CARTESIAN_POINT ( 'NONE',  ( 5.599999999999999645, -2.020725942163695166, -3.500000000000000000 ) ) ;
#15175=FACE_OUTER_BOUND ( 'NONE', #287, .T. ) ;
#15182=EDGE_CURVE ( 'NONE', #11132, #17929, #8157, .T. ) ;
#15197=CARTESIAN_POINT ( 'NONE',  ( 4.093692494532767512, -2.021783646005781421, -3.501831996793853374 ) ) ;
#15253=CARTESIAN_POINT ( 'NONE',  ( 25.15499999999999758, 0.000000000000000000, 2.500000000000000444 ) ) ;
#15263=EDGE_CURVE ( 'NONE', #18099, #10812, #9083, .T. ) ;
#15301=CARTESIAN_POINT ( 'NONE',  ( 4.175813232069148562, -2.061359961916374495, -3.570380186727398097 ) ) ;
#15322=EDGE_LOOP ( 'NONE', ( #1767, #8831, #12436 ) ) ;
#15338=CARTESIAN_POINT ( 'NONE',  ( 3.880206590543030742, 2.665671387532557279, 2.382921720510984276 ) ) ;
#15341=ORIENTED_EDGE ( 'NONE', *, *, #70, .T. ) ;
#15396=DIRECTION ( 'NONE',  ( 0.000000000000000000, 0.000000000000000000, -1.000000000000000000 ) ) ;
#15414=CARTESIAN_POINT ( 'NONE',  ( 4.093692494532766624, 2.021783646005775203, 3.501831996793853818 ) ) ;
#15422=CARTESIAN_POINT ( 'NONE',  ( 4.071447262713888016, 4.041451884327382338, 0.000000000000000000 ) ) ;
#15425=CARTESIAN_POINT ( 'NONE',  ( 4.175572532730930320, 2.061029303918049393, -3.569807470274390937 ) ) ;
#15442=CARTESIAN_POINT ( 'NONE',  ( 4.151274195509469855, 4.079825909417643004, -6.022632805413305277E-17 ) ) ;
#15443=ORIENTED_EDGE ( 'NONE', *, *, #3496, .F. ) ;
#15472=DIRECTION ( 'NONE',  ( -1.000000000000000000, -0.000000000000000000, -0.000000000000000000 ) ) ;
#15479=VECTOR ( 'NONE', #2457, 1000.000000000000000 ) ;
#15480=CARTESIAN_POINT ( 'NONE',  ( 4.050823680195223098, 2.400527758044901372, 2.978030508226147344 ) ) ;
#15486=( GEOMETRIC_REPRESENTATION_CONTEXT ( 3 ) GLOBAL_UNCERTAINTY_ASSIGNED_CONTEXT ( ( #9382 ) ) GLOBAL_UNIT_ASSIGNED_CONTEXT ( ( #7132, #16022, #5675 ) ) REPRESENTATION_CONTEXT ( 'NONE', 'WORKASPACE' ) );
#15492=VERTEX_POINT ( 'NONE', #17843 ) ;
#15494=CARTESIAN_POINT ( 'NONE',  ( 4.052424581287746186, -3.786734753435270662, -0.5771415817959170136 ) ) ;
#15515=ORIENTED_EDGE ( 'NONE', *, *, #6312, .F. ) ;
#15529=VECTOR ( 'NONE', #14766, 1000.000000000000000 ) ;
#15535=CIRCLE ( 'NONE', #14580, 0.4999999999999978351 ) ;
#15545=CARTESIAN_POINT ( 'NONE',  ( 4.175572532730932096, 4.122058607836115662, 6.089476485528261042E-15 ) ) ;
#15548=CARTESIAN_POINT ( 'NONE',  ( 0.000000000000000000, 0.000000000000000000, 0.000000000000000000 ) ) ;
#15553=CARTESIAN_POINT ( 'NONE',  ( 4.114405500665267112, -2.025575754679707075, 3.508400121684927431 ) ) ;
#15554=EDGE_LOOP ( 'NONE', ( #17876, #16697, #10566, #4646, #3140, #16798, #12149 ) ) ;
#15579=CARTESIAN_POINT ( 'NONE',  ( 4.086262418390198548, -2.102635014057360863, 3.500000000000000444 ) ) ;
#15595=CARTESIAN_POINT ( 'NONE',  ( 4.086376042167609413, -4.082715877136871008, 0.07147133206917888337 ) ) ;
#15648=CARTESIAN_POINT ( 'NONE',  ( 3.948103430090709409, -2.682758828852222166, 2.353325403973829388 ) ) ;
#15649=CARTESIAN_POINT ( 'NONE',  ( 4.175813232069147674, -2.061359961916367833, 3.570380186727398542 ) ) ;
#15665=CLOSED_SHELL ( 'NONE', ( #2295, #5230, #15976, #10438, #10230, #9259, #1821, #16046, #17956, #349, #14984, #5392, #2488, #1947, #3962, #4344, #19162, #14408, #14888, #12470, #10109, #434, #2925, #8744, #16563, #5653, #6246, #18609, #10986 ) ) ;
#15688=ORIENTED_EDGE ( 'NONE', *, *, #16573, .F. ) ;
#15695=EDGE_LOOP ( 'NONE', ( #3937, #4912, #13687, #374, #5032, #3500 ) ) ;
#15711=CARTESIAN_POINT ( 'NONE',  ( 4.132952817037859994, 2.031684012687258623, 3.518979934899746809 ) ) ;
#15734=CARTESIAN_POINT ( 'NONE',  ( 0.000000000000000000, 3.031088913245532979, -1.750000000000004219 ) ) ;
#15753=CARTESIAN_POINT ( 'NONE',  ( -7.538593230563273018E-17, 0.3423821193476820346, -3.499999999999999556 ) ) ;
#15838=VECTOR ( 'NONE', #11837, 1000.000000000000000 ) ;
#15841=CARTESIAN_POINT ( 'NONE',  ( 3.958484000407248793, -2.327740518748946386, 2.968235154690090472 ) ) ;
#15847=AXIS2_PLACEMENT_3D ( 'NONE', #12387, #4977, #10918 ) ;
#15855=CIRCLE ( 'NONE', #17724, 5.371010071662833063 ) ;
#15857=CARTESIAN_POINT ( 'NONE',  ( 0.3126073911696428675, 4.041451884327382338, -3.240528425403984455E-16 ) ) ;
#15873=CIRCLE ( 'NONE', #18373, 3.500000000000000000 ) ;
#15891=CARTESIAN_POINT ( 'NONE',  ( 4.086376042167605860, 1.979461949354204719, -3.571471332069179105 ) ) ;
#15899=CARTESIAN_POINT ( 'NONE',  ( 4.142654963991902584, 2.035398498734314554, 3.525413613457253792 ) ) ;
#15929=DIRECTION ( 'NONE',  ( 0.000000000000000000, -0.8660254037844380415, 0.5000000000000012212 ) ) ;
#15932=CARTESIAN_POINT ( 'NONE',  ( 4.180345304246197990, -2.049116244671344234, 3.591763845239310804 ) ) ;
#15933=CARTESIAN_POINT ( 'NONE',  ( 4.175075985190095373, -2.060370777630105454, 3.568666869285574084 ) ) ;
#15976=ADVANCED_FACE ( 'NONE', ( #3298 ), #14270, .T. ) ;
#16001=LINE ( 'NONE', #5562, #13654 ) ;
#16022=( NAMED_UNIT ( * ) PLANE_ANGLE_UNIT ( ) SI_UNIT ( $, .RADIAN. ) );
#16043=ORIENTED_EDGE ( 'NONE', *, *, #3012, .T. ) ;
#16046=ADVANCED_FACE ( 'NONE', ( #16787 ), #3400, .F. ) ;
#16049=CARTESIAN_POINT ( 'NONE',  ( 0.000000000000000000, 0.000000000000000000, 0.000000000000000000 ) ) ;
#16055=EDGE_CURVE ( 'NONE', #18944, #1594, #10029, .T. ) ;
#16061=CARTESIAN_POINT ( 'NONE',  ( 5.599999999999999645, 2.020725942163686728, -3.499999999999999556 ) ) ;
#16075=FACE_OUTER_BOUND ( 'NONE', #17301, .T. ) ;
#16180=CARTESIAN_POINT ( 'NONE',  ( 3.973110223765528914, 0.6902454861566582611, -3.565797985667391590 ) ) ;
#16185=CARTESIAN_POINT ( 'NONE',  ( 4.030867648404695025, 2.329326259788712772, -2.965488570641336974 ) ) ;
#16199=CARTESIAN_POINT ( 'NONE',  ( 4.071447262713890680, -4.041451884327388555, 0.000000000000000000 ) ) ;
#16276=CARTESIAN_POINT ( 'NONE',  ( 0.02993401039713966885, -3.373851915354620701, -1.156317065392240329 ) ) ;
#16309=FACE_OUTER_BOUND ( 'NONE', #11675, .T. ) ;
#16336=CARTESIAN_POINT ( 'NONE',  ( 4.630153689607048761, 0.000000000000000000, 0.000000000000000000 ) ) ;
#16342=ORIENTED_EDGE ( 'NONE', *, *, #7308, .F. ) ;
#16368=FACE_OUTER_BOUND ( 'NONE', #7139, .T. ) ;
#16383=CARTESIAN_POINT ( 'NONE',  ( 4.142654963991903472, -2.035398498734322104, -3.525413613457253348 ) ) ;
#16387=CARTESIAN_POINT ( 'NONE',  ( 3.950233766685291137, 0.7256672287179417591, -3.499999999999844125 ) ) ;
#16390=B_SPLINE_CURVE_WITH_KNOTS ( 'NONE', 3,
 ( #8832, #18029, #153, #14789 ),
 .UNSPECIFIED., .F., .F.,
 ( 4, 4 ),
 ( 2.380739282167303683E-07, 0.002044882221487525839 ),
 .UNSPECIFIED. ) ;
#16399=AXIS2_PLACEMENT_3D ( 'NONE', #10404, #14406, #6997 ) ;
#16411=ORIENTED_EDGE ( 'NONE', *, *, #3099, .F. ) ;
#16424=( LENGTH_UNIT ( ) NAMED_UNIT ( * ) SI_UNIT ( .MILLI., .METRE. ) );
#16428=AXIS2_PLACEMENT_3D ( 'NONE', #14751, #17596, #12909 ) ;
#16440=CARTESIAN_POINT ( 'NONE',  ( 0.1388410611046090037, -2.351840044243035610, 2.926493552096026018 ) ) ;
#16505=ORIENTED_EDGE ( 'NONE', *, *, #8987, .T. ) ;
#16514=CARTESIAN_POINT ( 'NONE',  ( 5.599999999999999645, 4.041451884327382338, 0.000000000000000000 ) ) ;
#16563=ADVANCED_FACE ( 'NONE', ( #6605 ), #3351, .F. ) ;
#16573=EDGE_CURVE ( 'NONE', #10162, #12012, #15535, .T. ) ;
#16584=CARTESIAN_POINT ( 'NONE',  ( 4.175813232069151226, -4.122719923832748101, -3.898053888241413974E-16 ) ) ;
#16598=ORIENTED_EDGE ( 'NONE', *, *, #17204, .T. ) ;
#16606=CARTESIAN_POINT ( 'NONE',  ( 4.170895651974600327, 2.054890354522691087, -3.559174498016439259 ) ) ;
#16608=CARTESIAN_POINT ( 'NONE',  ( 4.142654963991906136, -4.070796997468642431, 2.739218076410093718E-16 ) ) ;
#16632=EDGE_CURVE ( 'NONE', #7899, #12012, #9329, .T. ) ;
#16670=CARTESIAN_POINT ( 'NONE',  ( 4.033901012036491984, -2.321269032827139256, -2.979444097107483369 ) ) ;
#16678=CARTESIAN_POINT ( 'NONE',  ( 5.599999999999999645, 2.020725942163688504, 3.500000000000000000 ) ) ;
#16696=ORIENTED_EDGE ( 'NONE', *, *, #7308, .T. ) ;
#16697=ORIENTED_EDGE ( 'NONE', *, *, #16632, .T. ) ;
#16699=CARTESIAN_POINT ( 'NONE',  ( 4.071447262713887127, 2.020725942163686728, -3.499999999999999556 ) ) ;
#16700=DIRECTION ( 'NONE',  ( 0.000000000000000000, 0.5000000000000007772, -0.8660254037844381525 ) ) ;
#16712=CARTESIAN_POINT ( 'NONE',  ( 3.878096787214571517, 3.381939201670113082, 1.142309474598439234 ) ) ;
#16773=CARTESIAN_POINT ( 'NONE',  ( 0.000000000000000000, -3.031088913245531202, 1.750000000000006661 ) ) ;
#16781=LINE ( 'NONE', #9346, #7274 ) ;
#16783=FACE_OUTER_BOUND ( 'NONE', #336, .T. ) ;
#16784=DIRECTION ( 'NONE',  ( 0.000000000000000000, 0.000000000000000000, 1.000000000000000000 ) ) ;
#16787=FACE_OUTER_BOUND ( 'NONE', #9569, .T. ) ;
#16796=CARTESIAN_POINT ( 'NONE',  ( 3.951447005078451813, 2.357513599190969700, -2.916666666666668295 ) ) ;
#16798=ORIENTED_EDGE ( 'NONE', *, *, #290, .T. ) ;
#16806=CONICAL_SURFACE ( 'NONE', #6829, 5.371010071662833063, 1.221730476396037490 ) ;
#16809=EDGE_CURVE ( 'NONE', #5083, #18944, #8125, .T. ) ;
#16813=( NAMED_UNIT ( * ) SI_UNIT ( $, .STERADIAN. ) SOLID_ANGLE_UNIT ( ) );
#16825=FACE_OUTER_BOUND ( 'NONE', #6813, .T. ) ;
#16837=CARTESIAN_POINT ( 'NONE',  ( 0.03027795055833683302, 0.6888063905328593028, -3.499999999999998224 ) ) ;
#16896=ORIENTED_EDGE ( 'NONE', *, *, #913, .T. ) ;
#16916=CARTESIAN_POINT ( 'NONE',  ( 3.951447005078450925, 2.357513599190970144, 2.916666666666667407 ) ) ;
#16974=CARTESIAN_POINT ( 'NONE',  ( 0.3126073911696412022, -2.020725942163688504, 3.500000000000000444 ) ) ;
#16976=CARTESIAN_POINT ( 'NONE',  ( 4.124214193018024943, 2.028338413290970088, 3.513185186763604140 ) ) ;
#17010=UNCERTAINTY_MEASURE_WITH_UNIT (LENGTH_MEASURE( 1.000000000000000082E-05 ), #703, 'distance_accuracy_value', 'NONE');
#17014=CARTESIAN_POINT ( 'NONE',  ( 4.071447262713888016, -2.020725942163695166, -3.500000000000000000 ) ) ;
#17041=CARTESIAN_POINT ( 'NONE',  ( 3.974183935050569882, -0.7239581970533436328, 3.565826011443134380 ) ) ;
#17056=CARTESIAN_POINT ( 'NONE',  ( 5.100000000000002309, 0.000000000000000000, 5.200000000000001066 ) ) ;
#17087=ORIENTED_EDGE ( 'NONE', *, *, #3496, .T. ) ;
#17119=EDGE_CURVE ( 'NONE', #13429, #14350, #16001, .T. ) ;
#17139=CARTESIAN_POINT ( 'NONE',  ( 3.958491816110462747, 1.406739583089039902, 3.500000000000000000 ) ) ;
#17157=EDGE_CURVE ( 'NONE', #14350, #18754, #1507, .T. ) ;
#17159=ORIENTED_EDGE ( 'NONE', *, *, #4522, .F. ) ;
#17176=CARTESIAN_POINT ( 'NONE',  ( 4.170895651974599438, 2.054890354522711515, 3.559174498016425048 ) ) ;
#17178=LINE ( 'NONE', #12389, #12243 ) ;
#17204=EDGE_CURVE ( 'NONE', #7647, #2658, #11166, .T. ) ;
#17208=CARTESIAN_POINT ( 'NONE',  ( 4.158921614371307918, -1.986121848748765073, 3.559936047944508797 ) ) ;
#17209=CARTESIAN_POINT ( 'NONE',  ( 4.093692494532770176, -2.021783646005775203, 3.501831996793854707 ) ) ;
#17216=UNCERTAINTY_MEASURE_WITH_UNIT (LENGTH_MEASURE( 1.000000000000000082E-05 ), #16424, 'distance_accuracy_value', 'NONE');
#17232=ORIENTED_EDGE ( 'NONE', *, *, #18460, .F. ) ;
#17237=DIRECTION ( 'NONE',  ( -1.000000000000000000, -0.000000000000000000, -0.000000000000000000 ) ) ;
#17264=CARTESIAN_POINT ( 'NONE',  ( 3.958484000407027636, 2.327740518749021437, -2.968235154689955024 ) ) ;
#17290=DIRECTION ( 'NONE',  ( -1.000000000000000000, -0.000000000000000000, -0.000000000000000000 ) ) ;
#17301=EDGE_LOOP ( 'NONE', ( #16598, #3210, #9484 ) ) ;
#17304=CARTESIAN_POINT ( 'NONE',  ( 3.806834918298646731, 3.031088913245537864, 1.750000000000000666 ) ) ;
#17312=CARTESIAN_POINT ( 'NONE',  ( 0.1397371499203167999, 1.362866705341264417, 3.499999999999999556 ) ) ;
#17351=CARTESIAN_POINT ( 'NONE',  ( 25.15499999999999758, 0.000000000000000000, 0.000000000000000000 ) ) ;
#17358=CARTESIAN_POINT ( 'NONE',  ( 4.055492966679589806, 3.795017426214568168, -0.5629142681441285934 ) ) ;
#17367=ORIENTED_EDGE ( 'NONE', *, *, #6608, .F. ) ;
#17403=CARTESIAN_POINT ( 'NONE',  ( 4.180231891692623769, -4.134807952925581453, -0.02076457676760805685 ) ) ;
#17404=CARTESIAN_POINT ( 'NONE',  ( 4.082498951862918446, -2.020725942163687172, 3.500000000000002220 ) ) ;
#17416=CONICAL_SURFACE ( 'NONE', #4315, 3.500000000000000000, 1.047197551196600296 ) ;
#17426=CARTESIAN_POINT ( 'NONE',  ( 4.175813232069147674, -2.061359961916367833, 3.570380186727398542 ) ) ;
#17447=CARTESIAN_POINT ( 'NONE',  ( 3.951447005078451813, 1.347150628109125892, 3.500000000000000444 ) ) ;
#17462=CARTESIAN_POINT ( 'NONE',  ( 0.000000000000000000, -3.031088913245531202, 1.750000000000006661 ) ) ;
#17511=CARTESIAN_POINT ( 'NONE',  ( -1.959187206999195895E-15, 3.202582148906728765, 1.452965002680430828 ) ) ;
#17536=CARTESIAN_POINT ( 'NONE',  ( 3.972073812946708582, -0.6951863858492246528, -3.565770933504603057 ) ) ;
#17550=CARTESIAN_POINT ( 'NONE',  ( 4.052424581287633387, 2.393186648132967775, -2.990837702970182477 ) ) ;
#17561=CONICAL_SURFACE ( 'NONE', #9125, 2.055000000000000160, 0.7853981633974439491 ) ;
#17596=DIRECTION ( 'NONE',  ( 0.000000000000000000, 0.8660254037844375974, -0.5000000000000018874 ) ) ;
#17604=CARTESIAN_POINT ( 'NONE',  ( 0.000000000000000000, 3.031088913245533867, 1.750000000000002887 ) ) ;
#17615=ORIENTED_EDGE ( 'NONE', *, *, #10541, .T. ) ;
#17639=EDGE_LOOP ( 'NONE', ( #3257, #1465, #305, #7412, #1938 ) ) ;
#17682=( NAMED_UNIT ( * ) PLANE_ANGLE_UNIT ( ) SI_UNIT ( $, .RADIAN. ) );
#17687=EDGE_LOOP ( 'NONE', ( #13943, #17159, #17087, #1838 ) ) ;
#17694=CARTESIAN_POINT ( 'NONE',  ( 0.3126073911696408136, 2.020725942163688060, 3.500000000000000000 ) ) ;
#17709=CARTESIAN_POINT ( 'NONE',  ( 0.000000000000000000, 0.000000000000000000, 0.000000000000000000 ) ) ;
#17724=AXIS2_PLACEMENT_3D ( 'NONE', #16336, #11931, #10657 ) ;
#17725=CARTESIAN_POINT ( 'NONE',  ( 0.000000000000000000, 3.031088913245532979, -1.750000000000004219 ) ) ;
#17731=CIRCLE ( 'NONE', #12116, 0.4999999999999978351 ) ;
#17739=DIRECTION ( 'NONE',  ( -1.000000000000000000, -0.000000000000000000, -0.000000000000000000 ) ) ;
#17746=AXIS2_PLACEMENT_3D ( 'NONE', #7073, #19003, #4147 ) ;
#17749=DIRECTION ( 'NONE',  ( -1.000000000000000000, -0.000000000000000000, -0.000000000000000000 ) ) ;
#17751=CARTESIAN_POINT ( 'NONE',  ( 0.3126073911696412022, -2.020725942163688504, 3.500000000000000444 ) ) ;
#17840=DIRECTION ( 'NONE',  ( -1.000000000000000000, -0.000000000000000000, 0.000000000000000000 ) ) ;
#17843=CARTESIAN_POINT ( 'NONE',  ( 25.60000000000000142, 2.789133085058097101E-16, -2.055000000000000160 ) ) ;
#17848=ORIENTED_EDGE ( 'NONE', *, *, #15121, .T. ) ;
#17853=( BOUNDED_SURFACE ( )  B_SPLINE_SURFACE ( 3, 2, ( 
 ( #2940, #1480, #9990 ),
 ( #1093, #4606, #25 ),
 ( #15338, #10562, #12124 ),
 ( #16712, #219, #17897 ),
 ( #10842, #3319, #9280 ),
 ( #1860, #13579, #1954 ) ),
 .UNSPECIFIED., .F., .F., .T. ) 
 B_SPLINE_SURFACE_WITH_KNOTS ( ( 4, 2, 4 ),
 ( 3, 3 ),
 ( 0.01651999345535505245, 0.01858032176739834659, 0.02064065007944164074 ),
 ( 0.000000000000000000, 1.000000000000000000 ),
 .UNSPECIFIED. ) 
 GEOMETRIC_REPRESENTATION_ITEM ( )  RATIONAL_B_SPLINE_SURFACE ( (
 ( 1.000000000000000000, 0.8047781103519393575, 1.000000000000000000),
 ( 1.000000000000000000, 0.8123785825605439603, 1.000000000000000000),
 ( 1.000000000000000000, 0.8190671539786830158, 1.000000000000000000),
 ( 1.000000000000000000, 0.8192352254836331449, 1.000000000000000000),
 ( 1.000000000000000000, 0.8126129677210507385, 1.000000000000000000),
 ( 1.000000000000000000, 0.8047712537969728963, 1.000000000000000000) ) ) 
 REPRESENTATION_ITEM ( '' )  SURFACE ( )  );
#17872=MECHANICAL_DESIGN_GEOMETRIC_PRESENTATION_REPRESENTATION('',(#6011),#11629);
#17876=ORIENTED_EDGE ( 'NONE', *, *, #12122, .T. ) ;
#17896=( NAMED_UNIT ( * ) PLANE_ANGLE_UNIT ( ) SI_UNIT ( $, .RADIAN. ) );
#17897=CARTESIAN_POINT ( 'NONE',  ( 3.972066048304702779, 3.435565134476335380, 1.180968096049678229 ) ) ;
#17904=CARTESIAN_POINT ( 'NONE',  ( 0.3126073911696428675, 4.041451884327382338, -3.240528425403984455E-16 ) ) ;
#17929=VERTEX_POINT ( 'NONE', #9157 ) ;
#17955=FACE_OUTER_BOUND ( 'NONE', #18676, .T. ) ;
#17956=ADVANCED_FACE ( 'NONE', ( #16783 ), #16806, .T. ) ;
#17972=ORIENTED_EDGE ( 'NONE', *, *, #11143, .F. ) ;
#17982=AXIS2_PLACEMENT_3D ( 'NONE', #18043, #17840, #6218 ) ;
#17992=STYLED_ITEM ( 'NONE', ( #4009 ), #10882 ) ;
#18020=AXIS2_PLACEMENT_3D ( 'NONE', #18311, #15472, #8140 ) ;
#18029=CARTESIAN_POINT ( 'NONE',  ( 0.1217565302851095904, 2.351289329882149559, 2.927447417349536618 ) ) ;
#18043=CARTESIAN_POINT ( 'NONE',  ( 5.599999999999999645, 0.000000000000000000, 0.000000000000000000 ) ) ;
#18059=CARTESIAN_POINT ( 'NONE',  ( 0.000000000000000000, 0.000000000000000000, 0.000000000000000000 ) ) ;
#18081=CARTESIAN_POINT ( 'NONE',  ( 4.158413352280814657, 2.044871626972823986, -3.541821552872970180 ) ) ;
#18083=CARTESIAN_POINT ( 'NONE',  ( 5.100000000000002309, 0.000000000000000000, 0.000000000000000000 ) ) ;
#18097=EDGE_CURVE ( 'NONE', #10162, #11406, #14931, .T. ) ;
#18099=VERTEX_POINT ( 'NONE', #10107 ) ;
#18102=FACE_OUTER_BOUND ( 'NONE', #15322, .T. ) ;
#18106=ORIENTED_EDGE ( 'NONE', *, *, #6312, .T. ) ;
#18130=CARTESIAN_POINT ( 'NONE',  ( 0.1388410611046122789, -3.710337782248038785, -0.5735064479039801988 ) ) ;
#18139=( BOUNDED_SURFACE ( )  B_SPLINE_SURFACE ( 3, 2, ( 
 ( #15579, #8047, #14004 ),
 ( #642, #6592, #8336 ),
 ( #18510, #5128, #17041 ),
 ( #2190, #18608, #11172 ),
 ( #17139, #3744, #2280 ),
 ( #8244, #14195, #1467 ) ),
 .UNSPECIFIED., .F., .F., .F. ) 
 B_SPLINE_SURFACE_WITH_KNOTS ( ( 4, 2, 4 ),
 ( 3, 3 ),
 ( 0.01651732063679904258, 0.01857756227444016389, 0.02063780391208128520 ),
 ( 0.000000000000000000, 1.000000000000000000 ),
 .UNSPECIFIED. ) 
 GEOMETRIC_REPRESENTATION_ITEM ( )  RATIONAL_B_SPLINE_SURFACE ( (
 ( 1.000000000000000000, 0.8047781231227483234, 1.000000000000000000),
 ( 1.000000000000000000, 0.8123782108664980850, 1.000000000000000000),
 ( 1.000000000000000000, 0.8190665102133478648, 1.000000000000000000),
 ( 1.000000000000000000, 0.8192358432844011329, 1.000000000000000000),
 ( 1.000000000000000000, 0.8126132624435309371, 1.000000000000000000),
 ( 1.000000000000000000, 0.8047712436238877443, 1.000000000000000000) ) ) 
 REPRESENTATION_ITEM ( '' )  SURFACE ( )  );
#18143=CARTESIAN_POINT ( 'NONE',  ( 4.170895651974600327, -2.054890354522638685, -3.559174498016469457 ) ) ;
#18149=FACE_OUTER_BOUND ( 'NONE', #8951, .T. ) ;
#18174=ORIENTED_EDGE ( 'NONE', *, *, #11911, .F. ) ;
#18192=EDGE_CURVE ( 'NONE', #13276, #1546, #15873, .T. ) ;
#18293=ORIENTED_EDGE ( 'NONE', *, *, #1728, .T. ) ;
#18311=CARTESIAN_POINT ( 'NONE',  ( 5.100000000000002309, 0.000000000000000000, 0.000000000000000000 ) ) ;
#18333=ORIENTED_EDGE ( 'NONE', *, *, #7762, .T. ) ;
#18355=VECTOR ( 'NONE', #1090, 1000.000000000000114 ) ;
#18367=CARTESIAN_POINT ( 'NONE',  ( 4.165266963751927065, 2.049631966911918735, -3.550066703508781174 ) ) ;
#18369=FACE_OUTER_BOUND ( 'NONE', #8666, .T. ) ;
#18373=AXIS2_PLACEMENT_3D ( 'NONE', #12241, #9304, #1882 ) ;
#18384=CARTESIAN_POINT ( 'NONE',  ( 4.170895651974601215, 4.109780709045311120, -8.452559493485846499E-14 ) ) ;
#18387=CARTESIAN_POINT ( 'NONE',  ( 1.216174376970875689E-15, -2.686816014504582739, -2.346298152288355698 ) ) ;
#18390=ORIENTED_EDGE ( 'NONE', *, *, #8766, .T. ) ;
#18414=CARTESIAN_POINT ( 'NONE',  ( 4.175813232069148562, 4.122719923832742772, -5.545971589517866732E-16 ) ) ;
#18427=CARTESIAN_POINT ( 'NONE',  ( 4.030867648404662162, -3.732851566701945067, -0.5345114293593726806 ) ) ;
#18460=EDGE_CURVE ( 'NONE', #5869, #104, #12060, .T. ) ;
#18496=CARTESIAN_POINT ( 'NONE',  ( 4.071447262713888016, -2.020725942163695166, -3.500000000000000000 ) ) ;
#18510=CARTESIAN_POINT ( 'NONE',  ( 3.880214671983734043, -0.7309020039786090495, 3.500000000000000444 ) ) ;
#18522=EDGE_LOOP ( 'NONE', ( #4517, #14145, #1983 ) ) ;
#18528=DIRECTION ( 'NONE',  ( -1.000000000000000000, -0.000000000000000000, -0.000000000000000000 ) ) ;
#18532=DIRECTION ( 'NONE',  ( -0.000000000000000000, 0.000000000000000000, -1.000000000000000000 ) ) ;
#18541=DIRECTION ( 'NONE',  ( -1.000000000000000000, -0.000000000000000000, -0.000000000000000000 ) ) ;
#18545=ORIENTED_EDGE ( 'NONE', *, *, #1956, .F. ) ;
#18581=CARTESIAN_POINT ( 'NONE',  ( 5.599999999999998757, 0.000000000000000000, 0.000000000000000000 ) ) ;
#18585=ORIENTED_EDGE ( 'NONE', *, *, #8205, .F. ) ;
#18608=CARTESIAN_POINT ( 'NONE',  ( 3.948095570617042860, 0.6965071952231317587, 3.500000000000155875 ) ) ;
#18609=ADVANCED_FACE ( 'NONE', ( #11832 ), #17853, .F. ) ;
#18623=CARTESIAN_POINT ( 'NONE',  ( 4.158921614371310582, -4.076055977742311320, 0.05993604794450450857 ) ) ;
#18642=CARTESIAN_POINT ( 'NONE',  ( 4.175326769692871309, 2.060699556488903461, 3.569236330973477145 ) ) ;
#18650=AXIS2_PLACEMENT_3D ( 'NONE', #168, #10323, #8752 ) ;
#18654=EDGE_LOOP ( 'NONE', ( #8334, #16696, #3803, #6349 ) ) ;
#18676=EDGE_LOOP ( 'NONE', ( #16043, #17232, #641, #17367, #1105 ) ) ;
#18680=CARTESIAN_POINT ( 'NONE',  ( 4.052424581287801253, -2.393186648133309724, 2.990837702970520873 ) ) ;
#18682=CARTESIAN_POINT ( 'NONE',  ( 4.071447262713887127, -2.020725942163688060, 3.500000000000000444 ) ) ;
#18687=B_SPLINE_CURVE_WITH_KNOTS ( 'NONE', 3,
 ( #18846, #19032, #4082, #9952, #5467 ),
 .UNSPECIFIED., .F., .F.,
 ( 4, 1, 4 ),
 ( 0.000000000000000000, 0.002020725942163690506, 0.004041451884327381880 ),
 .UNSPECIFIED. ) ;
#18740=CARTESIAN_POINT ( 'NONE',  ( 0.3126073911696462537, -4.041451884327388555, -1.676097590879904329E-16 ) ) ;
#18754=VERTEX_POINT ( 'NONE', #1764 ) ;
#18788=ORIENTED_EDGE ( 'NONE', *, *, #14718, .T. ) ;
#18792=AXIS2_PLACEMENT_3D ( 'NONE', #18581, #12805, #993 ) ;
#18837=CARTESIAN_POINT ( 'NONE',  ( 1.067261513540418550E-16, -0.3420925509381367302, 3.500000000000000000 ) ) ;
#18846=CARTESIAN_POINT ( 'NONE',  ( 4.071447262713888016, -2.020725942163695166, -3.500000000000000000 ) ) ;
#18856=DIRECTION ( 'NONE',  ( 0.000000000000000000, 0.000000000000000000, 1.000000000000000000 ) ) ;
#18871=CARTESIAN_POINT ( 'NONE',  ( 3.950241966888154987, -3.393956070637305089, 1.121495646999519202 ) ) ;
#18893=FACE_OUTER_BOUND ( 'NONE', #2230, .T. ) ;
#18933=CARTESIAN_POINT ( 'NONE',  ( 4.158413352280808439, 2.044871626972822209, 3.541821552872961298 ) ) ;
#18944=VERTEX_POINT ( 'NONE', #12667 ) ;
#18969=CARTESIAN_POINT ( 'NONE',  ( 4.175326769692873974, -4.121399112977854884, -1.039526559595160114E-14 ) ) ;
#18974=AXIS2_PLACEMENT_3D ( 'NONE', #14612, #11877, #13531 ) ;
#19003=DIRECTION ( 'NONE',  ( -1.000000000000000000, -0.000000000000000000, -0.000000000000000000 ) ) ;
#19032=CARTESIAN_POINT ( 'NONE',  ( 3.951447005078451813, -2.357513599190978137, -2.916666666666667407 ) ) ;
#19053=FILL_AREA_STYLE ('',( #4102 ) ) ;
#19073=DIRECTION ( 'NONE',  ( -1.000000000000000000, -0.000000000000000000, 0.000000000000000000 ) ) ;
#19121=ORIENTED_EDGE ( 'NONE', *, *, #16573, .T. ) ;
#19129=CARTESIAN_POINT ( 'NONE',  ( 0.2175679805369840625, -1.691499766289389362, -3.500000000000000000 ) ) ;
#19160=CARTESIAN_POINT ( 'NONE',  ( 3.973514160553463626, -2.741076955031366502, -2.383932505289870996 ) ) ;
#19162=ADVANCED_FACE ( 'NONE', ( #13439 ), #4294, .T. ) ;
#19165=EDGE_CURVE ( 'NONE', #1546, #7647, #8697, .T. ) ;
#19210=CARTESIAN_POINT ( 'NONE',  ( 1.154929423581238118E-15, -3.202582148906733650, -1.452965002680433271 ) ) ;
#19226=ORIENTED_EDGE ( 'NONE', *, *, #7334, .T. ) ;
#19229=( GEOMETRIC_REPRESENTATION_CONTEXT ( 3 ) GLOBAL_UNCERTAINTY_ASSIGNED_CONTEXT ( ( #17010 ) ) GLOBAL_UNIT_ASSIGNED_CONTEXT ( ( #703, #17682, #8489 ) ) REPRESENTATION_CONTEXT ( 'NONE', 'WORKASPACE' ) );
#19240=CARTESIAN_POINT ( 'NONE',  ( 0.000000000000000000, 4.041451884327382338, 2.749426538070117193E-16 ) ) ;
#19243=PRODUCT_DEFINITION_FORMATION_WITH_SPECIFIED_SOURCE ( 'ANY', '', #11388, .NOT_KNOWN. ) ;
#19246=SURFACE_STYLE_FILL_AREA ( #19053 ) ;
#19270=DIRECTION ( 'NONE',  ( 0.000000000000000000, 0.000000000000000000, 1.000000000000000000 ) ) ;
#19312=CARTESIAN_POINT ( 'NONE',  ( 0.3126073911696462537, -4.041451884327388555, -1.676097590879904329E-16 ) ) ;
#19365=COLOUR_RGB('Black',0.12,0.14,0.17);
#19366=FILL_AREA_STYLE_COLOUR('',#19365);
#19367=FILL_AREA_STYLE('',(#19366));
#19368=SURFACE_STYLE_FILL_AREA(#19367);
#19369=SURFACE_SIDE_STYLE('',(#19368));
#19370=SURFACE_STYLE_USAGE(.BOTH.,#19369);
#19371=PRESENTATION_STYLE_ASSIGNMENT((#19370));
ENDSEC;
END-ISO-10303-21;
